ISO-10303-21;
HEADER;
/* Generated by software containing ST-Developer
 * from STEP Tools, Inc. (www.steptools.com) 
 */

FILE_DESCRIPTION(
/* description */ (''),
/* implementation_level */ '2;1');

FILE_NAME(
/* name */ '12_Spring_Pin_ISO_8752_4.76x12.step',
/* time_stamp */ '2026-10-25T01:30:15-07:00',
/* author */ (''),
/* organization */ (''),
/* preprocessor_version */ 'ST-DEVELOPER v20.2',
/* originating_system */ 'Autodesk Translation Framework v15.15.0.0',
/* authorisation */ '');

FILE_SCHEMA (('AUTOMOTIVE_DESIGN { 1 0 10303 214 3 1 1 }'));
ENDSEC;

DATA;
#10=MECHANICAL_DESIGN_GEOMETRIC_PRESENTATION_REPRESENTATION('',(#573),#32309);
#545=SHAPE_REPRESENTATION_RELATIONSHIP('SRR','None',#32372,#559);
#559=ADVANCED_BREP_SHAPE_REPRESENTATION('',(#587),#32305);
#573=STYLED_ITEM('',(#32502),#587);
#587=MANIFOLD_SOLID_BREP('Body1',#13814);
#1723=FACE_OUTER_BOUND('',#2573,.T.);
#1724=FACE_OUTER_BOUND('',#2574,.T.);
#1725=FACE_OUTER_BOUND('',#2575,.T.);
#1726=FACE_OUTER_BOUND('',#2576,.T.);
#1727=FACE_OUTER_BOUND('',#2577,.T.);
#1728=FACE_OUTER_BOUND('',#2578,.T.);
#1729=FACE_OUTER_BOUND('',#2579,.T.);
#1730=FACE_OUTER_BOUND('',#2580,.T.);
#1731=FACE_OUTER_BOUND('',#2581,.T.);
#1732=FACE_OUTER_BOUND('',#2582,.T.);
#1733=FACE_OUTER_BOUND('',#2583,.T.);
#1734=FACE_OUTER_BOUND('',#2584,.T.);
#1735=FACE_OUTER_BOUND('',#2585,.T.);
#1736=FACE_OUTER_BOUND('',#2586,.T.);
#1737=FACE_OUTER_BOUND('',#2587,.T.);
#1738=FACE_OUTER_BOUND('',#2588,.T.);
#1739=FACE_OUTER_BOUND('',#2589,.T.);
#1740=FACE_OUTER_BOUND('',#2590,.T.);
#1741=FACE_OUTER_BOUND('',#2591,.T.);
#1742=FACE_OUTER_BOUND('',#2592,.T.);
#1743=FACE_OUTER_BOUND('',#2593,.T.);
#1744=FACE_OUTER_BOUND('',#2594,.T.);
#1745=FACE_OUTER_BOUND('',#2595,.T.);
#1746=FACE_OUTER_BOUND('',#2596,.T.);
#1747=FACE_OUTER_BOUND('',#2597,.T.);
#1748=FACE_OUTER_BOUND('',#2598,.T.);
#1749=FACE_OUTER_BOUND('',#2599,.T.);
#1750=FACE_OUTER_BOUND('',#2600,.T.);
#1751=FACE_OUTER_BOUND('',#2601,.T.);
#1752=FACE_OUTER_BOUND('',#2602,.T.);
#1753=FACE_OUTER_BOUND('',#2603,.T.);
#1754=FACE_OUTER_BOUND('',#2604,.T.);
#1755=FACE_OUTER_BOUND('',#2605,.T.);
#1756=FACE_OUTER_BOUND('',#2606,.T.);
#1757=FACE_OUTER_BOUND('',#2607,.T.);
#1758=FACE_OUTER_BOUND('',#2608,.T.);
#1759=FACE_OUTER_BOUND('',#2609,.T.);
#1760=FACE_OUTER_BOUND('',#2610,.T.);
#1761=FACE_OUTER_BOUND('',#2611,.T.);
#1762=FACE_OUTER_BOUND('',#2612,.T.);
#1763=FACE_OUTER_BOUND('',#2613,.T.);
#1764=FACE_OUTER_BOUND('',#2614,.T.);
#1765=FACE_OUTER_BOUND('',#2615,.T.);
#1766=FACE_OUTER_BOUND('',#2616,.T.);
#1767=FACE_OUTER_BOUND('',#2617,.T.);
#1768=FACE_OUTER_BOUND('',#2618,.T.);
#1769=FACE_OUTER_BOUND('',#2619,.T.);
#1770=FACE_OUTER_BOUND('',#2620,.T.);
#1771=FACE_OUTER_BOUND('',#2621,.T.);
#1772=FACE_OUTER_BOUND('',#2622,.T.);
#1773=FACE_OUTER_BOUND('',#2623,.T.);
#1774=FACE_OUTER_BOUND('',#2624,.T.);
#2573=EDGE_LOOP('',(#10951,#10952,#10953,#10954));
#2574=EDGE_LOOP('',(#10955,#10956,#10957,#10958));
#2575=EDGE_LOOP('',(#10959,#10960,#10961,#10962));
#2576=EDGE_LOOP('',(#10963,#10964,#10965,#10966));
#2577=EDGE_LOOP('',(#10967,#10968,#10969,#10970));
#2578=EDGE_LOOP('',(#10971,#10972,#10973,#10974));
#2579=EDGE_LOOP('',(#10975,#10976,#10977,#10978));
#2580=EDGE_LOOP('',(#10979,#10980,#10981,#10982));
#2581=EDGE_LOOP('',(#10983,#10984,#10985,#10986));
#2582=EDGE_LOOP('',(#10987,#10988,#10989,#10990));
#2583=EDGE_LOOP('',(#10991,#10992,#10993,#10994));
#2584=EDGE_LOOP('',(#10995,#10996,#10997,#10998));
#2585=EDGE_LOOP('',(#10999,#11000,#11001,#11002));
#2586=EDGE_LOOP('',(#11003,#11004,#11005,#11006));
#2587=EDGE_LOOP('',(#11007,#11008,#11009,#11010));
#2588=EDGE_LOOP('',(#11011,#11012,#11013,#11014));
#2589=EDGE_LOOP('',(#11015,#11016,#11017,#11018));
#2590=EDGE_LOOP('',(#11019,#11020,#11021,#11022));
#2591=EDGE_LOOP('',(#11023,#11024,#11025,#11026));
#2592=EDGE_LOOP('',(#11027,#11028,#11029,#11030));
#2593=EDGE_LOOP('',(#11031,#11032,#11033,#11034));
#2594=EDGE_LOOP('',(#11035,#11036,#11037,#11038));
#2595=EDGE_LOOP('',(#11039,#11040,#11041,#11042));
#2596=EDGE_LOOP('',(#11043,#11044,#11045,#11046));
#2597=EDGE_LOOP('',(#11047,#11048,#11049,#11050));
#2598=EDGE_LOOP('',(#11051,#11052,#11053,#11054));
#2599=EDGE_LOOP('',(#11055,#11056,#11057,#11058));
#2600=EDGE_LOOP('',(#11059,#11060,#11061,#11062));
#2601=EDGE_LOOP('',(#11063,#11064,#11065,#11066));
#2602=EDGE_LOOP('',(#11067,#11068,#11069,#11070));
#2603=EDGE_LOOP('',(#11071,#11072,#11073,#11074));
#2604=EDGE_LOOP('',(#11075,#11076,#11077,#11078));
#2605=EDGE_LOOP('',(#11079,#11080,#11081,#11082));
#2606=EDGE_LOOP('',(#11083,#11084,#11085,#11086));
#2607=EDGE_LOOP('',(#11087,#11088,#11089,#11090));
#2608=EDGE_LOOP('',(#11091,#11092,#11093,#11094));
#2609=EDGE_LOOP('',(#11095,#11096,#11097,#11098));
#2610=EDGE_LOOP('',(#11099,#11100,#11101,#11102));
#2611=EDGE_LOOP('',(#11103,#11104,#11105,#11106));
#2612=EDGE_LOOP('',(#11107,#11108,#11109,#11110));
#2613=EDGE_LOOP('',(#11111,#11112,#11113,#11114));
#2614=EDGE_LOOP('',(#11115,#11116,#11117,#11118));
#2615=EDGE_LOOP('',(#11119,#11120,#11121,#11122));
#2616=EDGE_LOOP('',(#11123,#11124,#11125,#11126));
#2617=EDGE_LOOP('',(#11127,#11128,#11129,#11130));
#2618=EDGE_LOOP('',(#11131,#11132,#11133,#11134));
#2619=EDGE_LOOP('',(#11135,#11136,#11137,#11138));
#2620=EDGE_LOOP('',(#11139,#11140,#11141,#11142));
#2621=EDGE_LOOP('',(#11143,#11144,#11145,#11146));
#2622=EDGE_LOOP('',(#11147,#11148,#11149,#11150));
#2623=EDGE_LOOP('',(#11151,#11152,#11153,#11154,#11155,#11156,#11157,#11158,
#11159,#11160,#11161,#11162,#11163,#11164,#11165,#11166,#11167,#11168,#11169,
#11170,#11171,#11172,#11173,#11174,#11175,#11176,#11177,#11178,#11179,#11180,
#11181,#11182,#11183,#11184,#11185,#11186,#11187,#11188,#11189,#11190,#11191,
#11192,#11193,#11194,#11195,#11196,#11197,#11198,#11199,#11200));
#2624=EDGE_LOOP('',(#11201,#11202,#11203,#11204,#11205,#11206,#11207,#11208,
#11209,#11210,#11211,#11212,#11213,#11214,#11215,#11216,#11217,#11218,#11219,
#11220,#11221,#11222,#11223,#11224,#11225,#11226,#11227,#11228,#11229,#11230,
#11231,#11232,#11233,#11234,#11235,#11236,#11237,#11238,#11239,#11240,#11241,
#11242,#11243,#11244,#11245,#11246,#11247,#11248,#11249,#11250));
#3568=LINE('',#26545,#4879);
#3569=LINE('',#26547,#4880);
#3570=LINE('',#26549,#4881);
#3571=LINE('',#26550,#4882);
#3572=LINE('',#26553,#4883);
#3573=LINE('',#26555,#4884);
#3574=LINE('',#26556,#4885);
#3575=LINE('',#26559,#4886);
#3576=LINE('',#26561,#4887);
#3577=LINE('',#26562,#4888);
#3578=LINE('',#26565,#4889);
#3579=LINE('',#26567,#4890);
#3580=LINE('',#26568,#4891);
#3581=LINE('',#26571,#4892);
#3582=LINE('',#26573,#4893);
#3583=LINE('',#26574,#4894);
#3584=LINE('',#26577,#4895);
#3585=LINE('',#26579,#4896);
#3586=LINE('',#26580,#4897);
#3587=LINE('',#26583,#4898);
#3588=LINE('',#26585,#4899);
#3589=LINE('',#26586,#4900);
#3590=LINE('',#26589,#4901);
#3591=LINE('',#26591,#4902);
#3592=LINE('',#26592,#4903);
#3593=LINE('',#26595,#4904);
#3594=LINE('',#26597,#4905);
#3595=LINE('',#26598,#4906);
#3596=LINE('',#26601,#4907);
#3597=LINE('',#26603,#4908);
#3598=LINE('',#26604,#4909);
#3599=LINE('',#26607,#4910);
#3600=LINE('',#26609,#4911);
#3601=LINE('',#26610,#4912);
#3602=LINE('',#26613,#4913);
#3603=LINE('',#26615,#4914);
#3604=LINE('',#26616,#4915);
#3605=LINE('',#26619,#4916);
#3606=LINE('',#26621,#4917);
#3607=LINE('',#26622,#4918);
#3608=LINE('',#26625,#4919);
#3609=LINE('',#26627,#4920);
#3610=LINE('',#26628,#4921);
#3611=LINE('',#26631,#4922);
#3612=LINE('',#26633,#4923);
#3613=LINE('',#26634,#4924);
#3614=LINE('',#26637,#4925);
#3615=LINE('',#26639,#4926);
#3616=LINE('',#26640,#4927);
#3617=LINE('',#26643,#4928);
#3618=LINE('',#26645,#4929);
#3619=LINE('',#26646,#4930);
#3620=LINE('',#26649,#4931);
#3621=LINE('',#26651,#4932);
#3622=LINE('',#26652,#4933);
#3623=LINE('',#26655,#4934);
#3624=LINE('',#26657,#4935);
#3625=LINE('',#26658,#4936);
#3626=LINE('',#26661,#4937);
#3627=LINE('',#26663,#4938);
#3628=LINE('',#26664,#4939);
#3629=LINE('',#26667,#4940);
#3630=LINE('',#26669,#4941);
#3631=LINE('',#26670,#4942);
#3632=LINE('',#26673,#4943);
#3633=LINE('',#26675,#4944);
#3634=LINE('',#26676,#4945);
#3635=LINE('',#26679,#4946);
#3636=LINE('',#26681,#4947);
#3637=LINE('',#26682,#4948);
#3638=LINE('',#26685,#4949);
#3639=LINE('',#26687,#4950);
#3640=LINE('',#26688,#4951);
#3641=LINE('',#26691,#4952);
#3642=LINE('',#26693,#4953);
#3643=LINE('',#26694,#4954);
#3644=LINE('',#26697,#4955);
#3645=LINE('',#26699,#4956);
#3646=LINE('',#26700,#4957);
#3647=LINE('',#26703,#4958);
#3648=LINE('',#26705,#4959);
#3649=LINE('',#26706,#4960);
#3650=LINE('',#26709,#4961);
#3651=LINE('',#26711,#4962);
#3652=LINE('',#26712,#4963);
#3653=LINE('',#26715,#4964);
#3654=LINE('',#26717,#4965);
#3655=LINE('',#26718,#4966);
#3656=LINE('',#26721,#4967);
#3657=LINE('',#26723,#4968);
#3658=LINE('',#26724,#4969);
#3659=LINE('',#26727,#4970);
#3660=LINE('',#26729,#4971);
#3661=LINE('',#26730,#4972);
#3662=LINE('',#26733,#4973);
#3663=LINE('',#26735,#4974);
#3664=LINE('',#26736,#4975);
#3665=LINE('',#26739,#4976);
#3666=LINE('',#26741,#4977);
#3667=LINE('',#26742,#4978);
#3668=LINE('',#26745,#4979);
#3669=LINE('',#26747,#4980);
#3670=LINE('',#26748,#4981);
#3671=LINE('',#26751,#4982);
#3672=LINE('',#26753,#4983);
#3673=LINE('',#26754,#4984);
#3674=LINE('',#26757,#4985);
#3675=LINE('',#26759,#4986);
#3676=LINE('',#26760,#4987);
#3677=LINE('',#26763,#4988);
#3678=LINE('',#26765,#4989);
#3679=LINE('',#26766,#4990);
#3680=LINE('',#26769,#4991);
#3681=LINE('',#26771,#4992);
#3682=LINE('',#26772,#4993);
#3683=LINE('',#26775,#4994);
#3684=LINE('',#26777,#4995);
#3685=LINE('',#26778,#4996);
#3686=LINE('',#26781,#4997);
#3687=LINE('',#26783,#4998);
#3688=LINE('',#26784,#4999);
#3689=LINE('',#26787,#5000);
#3690=LINE('',#26789,#5001);
#3691=LINE('',#26790,#5002);
#3692=LINE('',#26793,#5003);
#3693=LINE('',#26795,#5004);
#3694=LINE('',#26796,#5005);
#3695=LINE('',#26799,#5006);
#3696=LINE('',#26801,#5007);
#3697=LINE('',#26802,#5008);
#3698=LINE('',#26805,#5009);
#3699=LINE('',#26807,#5010);
#3700=LINE('',#26808,#5011);
#3701=LINE('',#26811,#5012);
#3702=LINE('',#26813,#5013);
#3703=LINE('',#26814,#5014);
#3704=LINE('',#26817,#5015);
#3705=LINE('',#26819,#5016);
#3706=LINE('',#26820,#5017);
#3707=LINE('',#26823,#5018);
#3708=LINE('',#26825,#5019);
#3709=LINE('',#26826,#5020);
#3710=LINE('',#26829,#5021);
#3711=LINE('',#26831,#5022);
#3712=LINE('',#26832,#5023);
#3713=LINE('',#26835,#5024);
#3714=LINE('',#26837,#5025);
#3715=LINE('',#26838,#5026);
#3716=LINE('',#26840,#5027);
#3717=LINE('',#26841,#5028);
#4879=VECTOR('',#17008,10.);
#4880=VECTOR('',#17009,10.);
#4881=VECTOR('',#17010,10.);
#4882=VECTOR('',#17011,10.);
#4883=VECTOR('',#17014,10.);
#4884=VECTOR('',#17015,10.);
#4885=VECTOR('',#17016,10.);
#4886=VECTOR('',#17019,10.);
#4887=VECTOR('',#17020,10.);
#4888=VECTOR('',#17021,10.);
#4889=VECTOR('',#17024,10.);
#4890=VECTOR('',#17025,10.);
#4891=VECTOR('',#17026,10.);
#4892=VECTOR('',#17029,10.);
#4893=VECTOR('',#17030,10.);
#4894=VECTOR('',#17031,10.);
#4895=VECTOR('',#17034,10.);
#4896=VECTOR('',#17035,10.);
#4897=VECTOR('',#17036,10.);
#4898=VECTOR('',#17039,10.);
#4899=VECTOR('',#17040,10.);
#4900=VECTOR('',#17041,10.);
#4901=VECTOR('',#17044,10.);
#4902=VECTOR('',#17045,10.);
#4903=VECTOR('',#17046,10.);
#4904=VECTOR('',#17049,10.);
#4905=VECTOR('',#17050,10.);
#4906=VECTOR('',#17051,10.);
#4907=VECTOR('',#17054,10.);
#4908=VECTOR('',#17055,10.);
#4909=VECTOR('',#17056,10.);
#4910=VECTOR('',#17059,10.);
#4911=VECTOR('',#17060,10.);
#4912=VECTOR('',#17061,10.);
#4913=VECTOR('',#17064,10.);
#4914=VECTOR('',#17065,10.);
#4915=VECTOR('',#17066,10.);
#4916=VECTOR('',#17069,10.);
#4917=VECTOR('',#17070,10.);
#4918=VECTOR('',#17071,10.);
#4919=VECTOR('',#17074,10.);
#4920=VECTOR('',#17075,10.);
#4921=VECTOR('',#17076,10.);
#4922=VECTOR('',#17079,10.);
#4923=VECTOR('',#17080,10.);
#4924=VECTOR('',#17081,10.);
#4925=VECTOR('',#17084,10.);
#4926=VECTOR('',#17085,10.);
#4927=VECTOR('',#17086,10.);
#4928=VECTOR('',#17089,10.);
#4929=VECTOR('',#17090,10.);
#4930=VECTOR('',#17091,10.);
#4931=VECTOR('',#17094,10.);
#4932=VECTOR('',#17095,10.);
#4933=VECTOR('',#17096,10.);
#4934=VECTOR('',#17099,10.);
#4935=VECTOR('',#17100,10.);
#4936=VECTOR('',#17101,10.);
#4937=VECTOR('',#17104,10.);
#4938=VECTOR('',#17105,10.);
#4939=VECTOR('',#17106,10.);
#4940=VECTOR('',#17109,10.);
#4941=VECTOR('',#17110,10.);
#4942=VECTOR('',#17111,10.);
#4943=VECTOR('',#17114,10.);
#4944=VECTOR('',#17115,10.);
#4945=VECTOR('',#17116,10.);
#4946=VECTOR('',#17119,10.);
#4947=VECTOR('',#17120,10.);
#4948=VECTOR('',#17121,10.);
#4949=VECTOR('',#17124,10.);
#4950=VECTOR('',#17125,10.);
#4951=VECTOR('',#17126,10.);
#4952=VECTOR('',#17129,10.);
#4953=VECTOR('',#17130,10.);
#4954=VECTOR('',#17131,10.);
#4955=VECTOR('',#17134,10.);
#4956=VECTOR('',#17135,10.);
#4957=VECTOR('',#17136,10.);
#4958=VECTOR('',#17139,10.);
#4959=VECTOR('',#17140,10.);
#4960=VECTOR('',#17141,10.);
#4961=VECTOR('',#17144,10.);
#4962=VECTOR('',#17145,10.);
#4963=VECTOR('',#17146,10.);
#4964=VECTOR('',#17149,10.);
#4965=VECTOR('',#17150,10.);
#4966=VECTOR('',#17151,10.);
#4967=VECTOR('',#17154,10.);
#4968=VECTOR('',#17155,10.);
#4969=VECTOR('',#17156,10.);
#4970=VECTOR('',#17159,10.);
#4971=VECTOR('',#17160,10.);
#4972=VECTOR('',#17161,10.);
#4973=VECTOR('',#17164,10.);
#4974=VECTOR('',#17165,10.);
#4975=VECTOR('',#17166,10.);
#4976=VECTOR('',#17169,10.);
#4977=VECTOR('',#17170,10.);
#4978=VECTOR('',#17171,10.);
#4979=VECTOR('',#17174,10.);
#4980=VECTOR('',#17175,10.);
#4981=VECTOR('',#17176,10.);
#4982=VECTOR('',#17179,10.);
#4983=VECTOR('',#17180,10.);
#4984=VECTOR('',#17181,10.);
#4985=VECTOR('',#17184,10.);
#4986=VECTOR('',#17185,10.);
#4987=VECTOR('',#17186,10.);
#4988=VECTOR('',#17189,10.);
#4989=VECTOR('',#17190,10.);
#4990=VECTOR('',#17191,10.);
#4991=VECTOR('',#17194,10.);
#4992=VECTOR('',#17195,10.);
#4993=VECTOR('',#17196,10.);
#4994=VECTOR('',#17199,10.);
#4995=VECTOR('',#17200,10.);
#4996=VECTOR('',#17201,10.);
#4997=VECTOR('',#17204,10.);
#4998=VECTOR('',#17205,10.);
#4999=VECTOR('',#17206,10.);
#5000=VECTOR('',#17209,10.);
#5001=VECTOR('',#17210,10.);
#5002=VECTOR('',#17211,10.);
#5003=VECTOR('',#17214,10.);
#5004=VECTOR('',#17215,10.);
#5005=VECTOR('',#17216,10.);
#5006=VECTOR('',#17219,10.);
#5007=VECTOR('',#17220,10.);
#5008=VECTOR('',#17221,10.);
#5009=VECTOR('',#17224,10.);
#5010=VECTOR('',#17225,10.);
#5011=VECTOR('',#17226,10.);
#5012=VECTOR('',#17229,10.);
#5013=VECTOR('',#17230,10.);
#5014=VECTOR('',#17231,10.);
#5015=VECTOR('',#17234,10.);
#5016=VECTOR('',#17235,10.);
#5017=VECTOR('',#17236,10.);
#5018=VECTOR('',#17239,10.);
#5019=VECTOR('',#17240,10.);
#5020=VECTOR('',#17241,10.);
#5021=VECTOR('',#17244,10.);
#5022=VECTOR('',#17245,10.);
#5023=VECTOR('',#17246,10.);
#5024=VECTOR('',#17249,10.);
#5025=VECTOR('',#17250,10.);
#5026=VECTOR('',#17251,10.);
#5027=VECTOR('',#17254,10.);
#5028=VECTOR('',#17255,10.);
#6198=VERTEX_POINT('',#26543);
#6199=VERTEX_POINT('',#26544);
#6200=VERTEX_POINT('',#26546);
#6201=VERTEX_POINT('',#26548);
#6202=VERTEX_POINT('',#26552);
#6203=VERTEX_POINT('',#26554);
#6204=VERTEX_POINT('',#26558);
#6205=VERTEX_POINT('',#26560);
#6206=VERTEX_POINT('',#26564);
#6207=VERTEX_POINT('',#26566);
#6208=VERTEX_POINT('',#26570);
#6209=VERTEX_POINT('',#26572);
#6210=VERTEX_POINT('',#26576);
#6211=VERTEX_POINT('',#26578);
#6212=VERTEX_POINT('',#26582);
#6213=VERTEX_POINT('',#26584);
#6214=VERTEX_POINT('',#26588);
#6215=VERTEX_POINT('',#26590);
#6216=VERTEX_POINT('',#26594);
#6217=VERTEX_POINT('',#26596);
#6218=VERTEX_POINT('',#26600);
#6219=VERTEX_POINT('',#26602);
#6220=VERTEX_POINT('',#26606);
#6221=VERTEX_POINT('',#26608);
#6222=VERTEX_POINT('',#26612);
#6223=VERTEX_POINT('',#26614);
#6224=VERTEX_POINT('',#26618);
#6225=VERTEX_POINT('',#26620);
#6226=VERTEX_POINT('',#26624);
#6227=VERTEX_POINT('',#26626);
#6228=VERTEX_POINT('',#26630);
#6229=VERTEX_POINT('',#26632);
#6230=VERTEX_POINT('',#26636);
#6231=VERTEX_POINT('',#26638);
#6232=VERTEX_POINT('',#26642);
#6233=VERTEX_POINT('',#26644);
#6234=VERTEX_POINT('',#26648);
#6235=VERTEX_POINT('',#26650);
#6236=VERTEX_POINT('',#26654);
#6237=VERTEX_POINT('',#26656);
#6238=VERTEX_POINT('',#26660);
#6239=VERTEX_POINT('',#26662);
#6240=VERTEX_POINT('',#26666);
#6241=VERTEX_POINT('',#26668);
#6242=VERTEX_POINT('',#26672);
#6243=VERTEX_POINT('',#26674);
#6244=VERTEX_POINT('',#26678);
#6245=VERTEX_POINT('',#26680);
#6246=VERTEX_POINT('',#26684);
#6247=VERTEX_POINT('',#26686);
#6248=VERTEX_POINT('',#26690);
#6249=VERTEX_POINT('',#26692);
#6250=VERTEX_POINT('',#26696);
#6251=VERTEX_POINT('',#26698);
#6252=VERTEX_POINT('',#26702);
#6253=VERTEX_POINT('',#26704);
#6254=VERTEX_POINT('',#26708);
#6255=VERTEX_POINT('',#26710);
#6256=VERTEX_POINT('',#26714);
#6257=VERTEX_POINT('',#26716);
#6258=VERTEX_POINT('',#26720);
#6259=VERTEX_POINT('',#26722);
#6260=VERTEX_POINT('',#26726);
#6261=VERTEX_POINT('',#26728);
#6262=VERTEX_POINT('',#26732);
#6263=VERTEX_POINT('',#26734);
#6264=VERTEX_POINT('',#26738);
#6265=VERTEX_POINT('',#26740);
#6266=VERTEX_POINT('',#26744);
#6267=VERTEX_POINT('',#26746);
#6268=VERTEX_POINT('',#26750);
#6269=VERTEX_POINT('',#26752);
#6270=VERTEX_POINT('',#26756);
#6271=VERTEX_POINT('',#26758);
#6272=VERTEX_POINT('',#26762);
#6273=VERTEX_POINT('',#26764);
#6274=VERTEX_POINT('',#26768);
#6275=VERTEX_POINT('',#26770);
#6276=VERTEX_POINT('',#26774);
#6277=VERTEX_POINT('',#26776);
#6278=VERTEX_POINT('',#26780);
#6279=VERTEX_POINT('',#26782);
#6280=VERTEX_POINT('',#26786);
#6281=VERTEX_POINT('',#26788);
#6282=VERTEX_POINT('',#26792);
#6283=VERTEX_POINT('',#26794);
#6284=VERTEX_POINT('',#26798);
#6285=VERTEX_POINT('',#26800);
#6286=VERTEX_POINT('',#26804);
#6287=VERTEX_POINT('',#26806);
#6288=VERTEX_POINT('',#26810);
#6289=VERTEX_POINT('',#26812);
#6290=VERTEX_POINT('',#26816);
#6291=VERTEX_POINT('',#26818);
#6292=VERTEX_POINT('',#26822);
#6293=VERTEX_POINT('',#26824);
#6294=VERTEX_POINT('',#26828);
#6295=VERTEX_POINT('',#26830);
#6296=VERTEX_POINT('',#26834);
#6297=VERTEX_POINT('',#26836);
#7852=EDGE_CURVE('',#6198,#6199,#3568,.T.);
#7853=EDGE_CURVE('',#6199,#6200,#3569,.T.);
#7854=EDGE_CURVE('',#6201,#6200,#3570,.T.);
#7855=EDGE_CURVE('',#6198,#6201,#3571,.T.);
#7856=EDGE_CURVE('',#6202,#6198,#3572,.T.);
#7857=EDGE_CURVE('',#6203,#6201,#3573,.T.);
#7858=EDGE_CURVE('',#6202,#6203,#3574,.T.);
#7859=EDGE_CURVE('',#6204,#6202,#3575,.T.);
#7860=EDGE_CURVE('',#6205,#6203,#3576,.T.);
#7861=EDGE_CURVE('',#6204,#6205,#3577,.T.);
#7862=EDGE_CURVE('',#6206,#6204,#3578,.T.);
#7863=EDGE_CURVE('',#6207,#6205,#3579,.T.);
#7864=EDGE_CURVE('',#6206,#6207,#3580,.T.);
#7865=EDGE_CURVE('',#6208,#6206,#3581,.T.);
#7866=EDGE_CURVE('',#6209,#6207,#3582,.T.);
#7867=EDGE_CURVE('',#6208,#6209,#3583,.T.);
#7868=EDGE_CURVE('',#6210,#6208,#3584,.T.);
#7869=EDGE_CURVE('',#6211,#6209,#3585,.T.);
#7870=EDGE_CURVE('',#6210,#6211,#3586,.T.);
#7871=EDGE_CURVE('',#6212,#6210,#3587,.T.);
#7872=EDGE_CURVE('',#6213,#6211,#3588,.T.);
#7873=EDGE_CURVE('',#6212,#6213,#3589,.T.);
#7874=EDGE_CURVE('',#6214,#6212,#3590,.T.);
#7875=EDGE_CURVE('',#6215,#6213,#3591,.T.);
#7876=EDGE_CURVE('',#6214,#6215,#3592,.T.);
#7877=EDGE_CURVE('',#6216,#6214,#3593,.T.);
#7878=EDGE_CURVE('',#6217,#6215,#3594,.T.);
#7879=EDGE_CURVE('',#6216,#6217,#3595,.T.);
#7880=EDGE_CURVE('',#6218,#6216,#3596,.T.);
#7881=EDGE_CURVE('',#6219,#6217,#3597,.T.);
#7882=EDGE_CURVE('',#6218,#6219,#3598,.T.);
#7883=EDGE_CURVE('',#6220,#6218,#3599,.T.);
#7884=EDGE_CURVE('',#6221,#6219,#3600,.T.);
#7885=EDGE_CURVE('',#6220,#6221,#3601,.T.);
#7886=EDGE_CURVE('',#6222,#6220,#3602,.T.);
#7887=EDGE_CURVE('',#6223,#6221,#3603,.T.);
#7888=EDGE_CURVE('',#6222,#6223,#3604,.T.);
#7889=EDGE_CURVE('',#6224,#6222,#3605,.T.);
#7890=EDGE_CURVE('',#6225,#6223,#3606,.T.);
#7891=EDGE_CURVE('',#6224,#6225,#3607,.T.);
#7892=EDGE_CURVE('',#6226,#6224,#3608,.T.);
#7893=EDGE_CURVE('',#6227,#6225,#3609,.T.);
#7894=EDGE_CURVE('',#6226,#6227,#3610,.T.);
#7895=EDGE_CURVE('',#6228,#6226,#3611,.T.);
#7896=EDGE_CURVE('',#6229,#6227,#3612,.T.);
#7897=EDGE_CURVE('',#6228,#6229,#3613,.T.);
#7898=EDGE_CURVE('',#6230,#6228,#3614,.T.);
#7899=EDGE_CURVE('',#6231,#6229,#3615,.T.);
#7900=EDGE_CURVE('',#6230,#6231,#3616,.T.);
#7901=EDGE_CURVE('',#6232,#6230,#3617,.T.);
#7902=EDGE_CURVE('',#6233,#6231,#3618,.T.);
#7903=EDGE_CURVE('',#6232,#6233,#3619,.T.);
#7904=EDGE_CURVE('',#6234,#6232,#3620,.T.);
#7905=EDGE_CURVE('',#6235,#6233,#3621,.T.);
#7906=EDGE_CURVE('',#6234,#6235,#3622,.T.);
#7907=EDGE_CURVE('',#6236,#6234,#3623,.T.);
#7908=EDGE_CURVE('',#6237,#6235,#3624,.T.);
#7909=EDGE_CURVE('',#6236,#6237,#3625,.T.);
#7910=EDGE_CURVE('',#6238,#6236,#3626,.T.);
#7911=EDGE_CURVE('',#6239,#6237,#3627,.T.);
#7912=EDGE_CURVE('',#6238,#6239,#3628,.T.);
#7913=EDGE_CURVE('',#6240,#6238,#3629,.T.);
#7914=EDGE_CURVE('',#6241,#6239,#3630,.T.);
#7915=EDGE_CURVE('',#6240,#6241,#3631,.T.);
#7916=EDGE_CURVE('',#6242,#6240,#3632,.T.);
#7917=EDGE_CURVE('',#6243,#6241,#3633,.T.);
#7918=EDGE_CURVE('',#6242,#6243,#3634,.T.);
#7919=EDGE_CURVE('',#6244,#6242,#3635,.T.);
#7920=EDGE_CURVE('',#6245,#6243,#3636,.T.);
#7921=EDGE_CURVE('',#6244,#6245,#3637,.T.);
#7922=EDGE_CURVE('',#6246,#6244,#3638,.T.);
#7923=EDGE_CURVE('',#6247,#6245,#3639,.T.);
#7924=EDGE_CURVE('',#6246,#6247,#3640,.T.);
#7925=EDGE_CURVE('',#6248,#6246,#3641,.T.);
#7926=EDGE_CURVE('',#6249,#6247,#3642,.T.);
#7927=EDGE_CURVE('',#6248,#6249,#3643,.T.);
#7928=EDGE_CURVE('',#6250,#6248,#3644,.T.);
#7929=EDGE_CURVE('',#6251,#6249,#3645,.T.);
#7930=EDGE_CURVE('',#6250,#6251,#3646,.T.);
#7931=EDGE_CURVE('',#6252,#6250,#3647,.T.);
#7932=EDGE_CURVE('',#6253,#6251,#3648,.T.);
#7933=EDGE_CURVE('',#6252,#6253,#3649,.T.);
#7934=EDGE_CURVE('',#6254,#6252,#3650,.T.);
#7935=EDGE_CURVE('',#6255,#6253,#3651,.T.);
#7936=EDGE_CURVE('',#6254,#6255,#3652,.T.);
#7937=EDGE_CURVE('',#6256,#6254,#3653,.T.);
#7938=EDGE_CURVE('',#6257,#6255,#3654,.T.);
#7939=EDGE_CURVE('',#6256,#6257,#3655,.T.);
#7940=EDGE_CURVE('',#6258,#6256,#3656,.T.);
#7941=EDGE_CURVE('',#6259,#6257,#3657,.T.);
#7942=EDGE_CURVE('',#6258,#6259,#3658,.T.);
#7943=EDGE_CURVE('',#6260,#6258,#3659,.T.);
#7944=EDGE_CURVE('',#6261,#6259,#3660,.T.);
#7945=EDGE_CURVE('',#6260,#6261,#3661,.T.);
#7946=EDGE_CURVE('',#6262,#6260,#3662,.T.);
#7947=EDGE_CURVE('',#6263,#6261,#3663,.T.);
#7948=EDGE_CURVE('',#6262,#6263,#3664,.T.);
#7949=EDGE_CURVE('',#6264,#6262,#3665,.T.);
#7950=EDGE_CURVE('',#6265,#6263,#3666,.T.);
#7951=EDGE_CURVE('',#6264,#6265,#3667,.T.);
#7952=EDGE_CURVE('',#6266,#6264,#3668,.T.);
#7953=EDGE_CURVE('',#6267,#6265,#3669,.T.);
#7954=EDGE_CURVE('',#6266,#6267,#3670,.T.);
#7955=EDGE_CURVE('',#6268,#6266,#3671,.T.);
#7956=EDGE_CURVE('',#6269,#6267,#3672,.T.);
#7957=EDGE_CURVE('',#6268,#6269,#3673,.T.);
#7958=EDGE_CURVE('',#6270,#6268,#3674,.T.);
#7959=EDGE_CURVE('',#6271,#6269,#3675,.T.);
#7960=EDGE_CURVE('',#6270,#6271,#3676,.T.);
#7961=EDGE_CURVE('',#6272,#6270,#3677,.T.);
#7962=EDGE_CURVE('',#6273,#6271,#3678,.T.);
#7963=EDGE_CURVE('',#6272,#6273,#3679,.T.);
#7964=EDGE_CURVE('',#6274,#6272,#3680,.T.);
#7965=EDGE_CURVE('',#6275,#6273,#3681,.T.);
#7966=EDGE_CURVE('',#6274,#6275,#3682,.T.);
#7967=EDGE_CURVE('',#6276,#6274,#3683,.T.);
#7968=EDGE_CURVE('',#6277,#6275,#3684,.T.);
#7969=EDGE_CURVE('',#6276,#6277,#3685,.T.);
#7970=EDGE_CURVE('',#6278,#6276,#3686,.T.);
#7971=EDGE_CURVE('',#6279,#6277,#3687,.T.);
#7972=EDGE_CURVE('',#6278,#6279,#3688,.T.);
#7973=EDGE_CURVE('',#6280,#6278,#3689,.T.);
#7974=EDGE_CURVE('',#6281,#6279,#3690,.T.);
#7975=EDGE_CURVE('',#6280,#6281,#3691,.T.);
#7976=EDGE_CURVE('',#6282,#6280,#3692,.T.);
#7977=EDGE_CURVE('',#6283,#6281,#3693,.T.);
#7978=EDGE_CURVE('',#6282,#6283,#3694,.T.);
#7979=EDGE_CURVE('',#6284,#6282,#3695,.T.);
#7980=EDGE_CURVE('',#6285,#6283,#3696,.T.);
#7981=EDGE_CURVE('',#6284,#6285,#3697,.T.);
#7982=EDGE_CURVE('',#6286,#6284,#3698,.T.);
#7983=EDGE_CURVE('',#6287,#6285,#3699,.T.);
#7984=EDGE_CURVE('',#6286,#6287,#3700,.T.);
#7985=EDGE_CURVE('',#6288,#6286,#3701,.T.);
#7986=EDGE_CURVE('',#6289,#6287,#3702,.T.);
#7987=EDGE_CURVE('',#6288,#6289,#3703,.T.);
#7988=EDGE_CURVE('',#6290,#6288,#3704,.T.);
#7989=EDGE_CURVE('',#6291,#6289,#3705,.T.);
#7990=EDGE_CURVE('',#6290,#6291,#3706,.T.);
#7991=EDGE_CURVE('',#6292,#6290,#3707,.T.);
#7992=EDGE_CURVE('',#6293,#6291,#3708,.T.);
#7993=EDGE_CURVE('',#6292,#6293,#3709,.T.);
#7994=EDGE_CURVE('',#6294,#6292,#3710,.T.);
#7995=EDGE_CURVE('',#6295,#6293,#3711,.T.);
#7996=EDGE_CURVE('',#6294,#6295,#3712,.T.);
#7997=EDGE_CURVE('',#6296,#6294,#3713,.T.);
#7998=EDGE_CURVE('',#6297,#6295,#3714,.T.);
#7999=EDGE_CURVE('',#6296,#6297,#3715,.T.);
#8000=EDGE_CURVE('',#6199,#6296,#3716,.T.);
#8001=EDGE_CURVE('',#6200,#6297,#3717,.T.);
#10951=ORIENTED_EDGE('',*,*,#7852,.T.);
#10952=ORIENTED_EDGE('',*,*,#7853,.T.);
#10953=ORIENTED_EDGE('',*,*,#7854,.F.);
#10954=ORIENTED_EDGE('',*,*,#7855,.F.);
#10955=ORIENTED_EDGE('',*,*,#7856,.T.);
#10956=ORIENTED_EDGE('',*,*,#7855,.T.);
#10957=ORIENTED_EDGE('',*,*,#7857,.F.);
#10958=ORIENTED_EDGE('',*,*,#7858,.F.);
#10959=ORIENTED_EDGE('',*,*,#7859,.T.);
#10960=ORIENTED_EDGE('',*,*,#7858,.T.);
#10961=ORIENTED_EDGE('',*,*,#7860,.F.);
#10962=ORIENTED_EDGE('',*,*,#7861,.F.);
#10963=ORIENTED_EDGE('',*,*,#7862,.T.);
#10964=ORIENTED_EDGE('',*,*,#7861,.T.);
#10965=ORIENTED_EDGE('',*,*,#7863,.F.);
#10966=ORIENTED_EDGE('',*,*,#7864,.F.);
#10967=ORIENTED_EDGE('',*,*,#7865,.T.);
#10968=ORIENTED_EDGE('',*,*,#7864,.T.);
#10969=ORIENTED_EDGE('',*,*,#7866,.F.);
#10970=ORIENTED_EDGE('',*,*,#7867,.F.);
#10971=ORIENTED_EDGE('',*,*,#7868,.T.);
#10972=ORIENTED_EDGE('',*,*,#7867,.T.);
#10973=ORIENTED_EDGE('',*,*,#7869,.F.);
#10974=ORIENTED_EDGE('',*,*,#7870,.F.);
#10975=ORIENTED_EDGE('',*,*,#7871,.T.);
#10976=ORIENTED_EDGE('',*,*,#7870,.T.);
#10977=ORIENTED_EDGE('',*,*,#7872,.F.);
#10978=ORIENTED_EDGE('',*,*,#7873,.F.);
#10979=ORIENTED_EDGE('',*,*,#7874,.T.);
#10980=ORIENTED_EDGE('',*,*,#7873,.T.);
#10981=ORIENTED_EDGE('',*,*,#7875,.F.);
#10982=ORIENTED_EDGE('',*,*,#7876,.F.);
#10983=ORIENTED_EDGE('',*,*,#7877,.T.);
#10984=ORIENTED_EDGE('',*,*,#7876,.T.);
#10985=ORIENTED_EDGE('',*,*,#7878,.F.);
#10986=ORIENTED_EDGE('',*,*,#7879,.F.);
#10987=ORIENTED_EDGE('',*,*,#7880,.T.);
#10988=ORIENTED_EDGE('',*,*,#7879,.T.);
#10989=ORIENTED_EDGE('',*,*,#7881,.F.);
#10990=ORIENTED_EDGE('',*,*,#7882,.F.);
#10991=ORIENTED_EDGE('',*,*,#7883,.T.);
#10992=ORIENTED_EDGE('',*,*,#7882,.T.);
#10993=ORIENTED_EDGE('',*,*,#7884,.F.);
#10994=ORIENTED_EDGE('',*,*,#7885,.F.);
#10995=ORIENTED_EDGE('',*,*,#7886,.T.);
#10996=ORIENTED_EDGE('',*,*,#7885,.T.);
#10997=ORIENTED_EDGE('',*,*,#7887,.F.);
#10998=ORIENTED_EDGE('',*,*,#7888,.F.);
#10999=ORIENTED_EDGE('',*,*,#7889,.T.);
#11000=ORIENTED_EDGE('',*,*,#7888,.T.);
#11001=ORIENTED_EDGE('',*,*,#7890,.F.);
#11002=ORIENTED_EDGE('',*,*,#7891,.F.);
#11003=ORIENTED_EDGE('',*,*,#7892,.T.);
#11004=ORIENTED_EDGE('',*,*,#7891,.T.);
#11005=ORIENTED_EDGE('',*,*,#7893,.F.);
#11006=ORIENTED_EDGE('',*,*,#7894,.F.);
#11007=ORIENTED_EDGE('',*,*,#7895,.T.);
#11008=ORIENTED_EDGE('',*,*,#7894,.T.);
#11009=ORIENTED_EDGE('',*,*,#7896,.F.);
#11010=ORIENTED_EDGE('',*,*,#7897,.F.);
#11011=ORIENTED_EDGE('',*,*,#7898,.T.);
#11012=ORIENTED_EDGE('',*,*,#7897,.T.);
#11013=ORIENTED_EDGE('',*,*,#7899,.F.);
#11014=ORIENTED_EDGE('',*,*,#7900,.F.);
#11015=ORIENTED_EDGE('',*,*,#7901,.T.);
#11016=ORIENTED_EDGE('',*,*,#7900,.T.);
#11017=ORIENTED_EDGE('',*,*,#7902,.F.);
#11018=ORIENTED_EDGE('',*,*,#7903,.F.);
#11019=ORIENTED_EDGE('',*,*,#7904,.T.);
#11020=ORIENTED_EDGE('',*,*,#7903,.T.);
#11021=ORIENTED_EDGE('',*,*,#7905,.F.);
#11022=ORIENTED_EDGE('',*,*,#7906,.F.);
#11023=ORIENTED_EDGE('',*,*,#7907,.T.);
#11024=ORIENTED_EDGE('',*,*,#7906,.T.);
#11025=ORIENTED_EDGE('',*,*,#7908,.F.);
#11026=ORIENTED_EDGE('',*,*,#7909,.F.);
#11027=ORIENTED_EDGE('',*,*,#7910,.T.);
#11028=ORIENTED_EDGE('',*,*,#7909,.T.);
#11029=ORIENTED_EDGE('',*,*,#7911,.F.);
#11030=ORIENTED_EDGE('',*,*,#7912,.F.);
#11031=ORIENTED_EDGE('',*,*,#7913,.T.);
#11032=ORIENTED_EDGE('',*,*,#7912,.T.);
#11033=ORIENTED_EDGE('',*,*,#7914,.F.);
#11034=ORIENTED_EDGE('',*,*,#7915,.F.);
#11035=ORIENTED_EDGE('',*,*,#7916,.T.);
#11036=ORIENTED_EDGE('',*,*,#7915,.T.);
#11037=ORIENTED_EDGE('',*,*,#7917,.F.);
#11038=ORIENTED_EDGE('',*,*,#7918,.F.);
#11039=ORIENTED_EDGE('',*,*,#7919,.T.);
#11040=ORIENTED_EDGE('',*,*,#7918,.T.);
#11041=ORIENTED_EDGE('',*,*,#7920,.F.);
#11042=ORIENTED_EDGE('',*,*,#7921,.F.);
#11043=ORIENTED_EDGE('',*,*,#7922,.T.);
#11044=ORIENTED_EDGE('',*,*,#7921,.T.);
#11045=ORIENTED_EDGE('',*,*,#7923,.F.);
#11046=ORIENTED_EDGE('',*,*,#7924,.F.);
#11047=ORIENTED_EDGE('',*,*,#7925,.T.);
#11048=ORIENTED_EDGE('',*,*,#7924,.T.);
#11049=ORIENTED_EDGE('',*,*,#7926,.F.);
#11050=ORIENTED_EDGE('',*,*,#7927,.F.);
#11051=ORIENTED_EDGE('',*,*,#7928,.T.);
#11052=ORIENTED_EDGE('',*,*,#7927,.T.);
#11053=ORIENTED_EDGE('',*,*,#7929,.F.);
#11054=ORIENTED_EDGE('',*,*,#7930,.F.);
#11055=ORIENTED_EDGE('',*,*,#7931,.T.);
#11056=ORIENTED_EDGE('',*,*,#7930,.T.);
#11057=ORIENTED_EDGE('',*,*,#7932,.F.);
#11058=ORIENTED_EDGE('',*,*,#7933,.F.);
#11059=ORIENTED_EDGE('',*,*,#7934,.T.);
#11060=ORIENTED_EDGE('',*,*,#7933,.T.);
#11061=ORIENTED_EDGE('',*,*,#7935,.F.);
#11062=ORIENTED_EDGE('',*,*,#7936,.F.);
#11063=ORIENTED_EDGE('',*,*,#7937,.T.);
#11064=ORIENTED_EDGE('',*,*,#7936,.T.);
#11065=ORIENTED_EDGE('',*,*,#7938,.F.);
#11066=ORIENTED_EDGE('',*,*,#7939,.F.);
#11067=ORIENTED_EDGE('',*,*,#7940,.T.);
#11068=ORIENTED_EDGE('',*,*,#7939,.T.);
#11069=ORIENTED_EDGE('',*,*,#7941,.F.);
#11070=ORIENTED_EDGE('',*,*,#7942,.F.);
#11071=ORIENTED_EDGE('',*,*,#7943,.T.);
#11072=ORIENTED_EDGE('',*,*,#7942,.T.);
#11073=ORIENTED_EDGE('',*,*,#7944,.F.);
#11074=ORIENTED_EDGE('',*,*,#7945,.F.);
#11075=ORIENTED_EDGE('',*,*,#7946,.T.);
#11076=ORIENTED_EDGE('',*,*,#7945,.T.);
#11077=ORIENTED_EDGE('',*,*,#7947,.F.);
#11078=ORIENTED_EDGE('',*,*,#7948,.F.);
#11079=ORIENTED_EDGE('',*,*,#7949,.T.);
#11080=ORIENTED_EDGE('',*,*,#7948,.T.);
#11081=ORIENTED_EDGE('',*,*,#7950,.F.);
#11082=ORIENTED_EDGE('',*,*,#7951,.F.);
#11083=ORIENTED_EDGE('',*,*,#7952,.T.);
#11084=ORIENTED_EDGE('',*,*,#7951,.T.);
#11085=ORIENTED_EDGE('',*,*,#7953,.F.);
#11086=ORIENTED_EDGE('',*,*,#7954,.F.);
#11087=ORIENTED_EDGE('',*,*,#7955,.T.);
#11088=ORIENTED_EDGE('',*,*,#7954,.T.);
#11089=ORIENTED_EDGE('',*,*,#7956,.F.);
#11090=ORIENTED_EDGE('',*,*,#7957,.F.);
#11091=ORIENTED_EDGE('',*,*,#7958,.T.);
#11092=ORIENTED_EDGE('',*,*,#7957,.T.);
#11093=ORIENTED_EDGE('',*,*,#7959,.F.);
#11094=ORIENTED_EDGE('',*,*,#7960,.F.);
#11095=ORIENTED_EDGE('',*,*,#7961,.T.);
#11096=ORIENTED_EDGE('',*,*,#7960,.T.);
#11097=ORIENTED_EDGE('',*,*,#7962,.F.);
#11098=ORIENTED_EDGE('',*,*,#7963,.F.);
#11099=ORIENTED_EDGE('',*,*,#7964,.T.);
#11100=ORIENTED_EDGE('',*,*,#7963,.T.);
#11101=ORIENTED_EDGE('',*,*,#7965,.F.);
#11102=ORIENTED_EDGE('',*,*,#7966,.F.);
#11103=ORIENTED_EDGE('',*,*,#7967,.T.);
#11104=ORIENTED_EDGE('',*,*,#7966,.T.);
#11105=ORIENTED_EDGE('',*,*,#7968,.F.);
#11106=ORIENTED_EDGE('',*,*,#7969,.F.);
#11107=ORIENTED_EDGE('',*,*,#7970,.T.);
#11108=ORIENTED_EDGE('',*,*,#7969,.T.);
#11109=ORIENTED_EDGE('',*,*,#7971,.F.);
#11110=ORIENTED_EDGE('',*,*,#7972,.F.);
#11111=ORIENTED_EDGE('',*,*,#7973,.T.);
#11112=ORIENTED_EDGE('',*,*,#7972,.T.);
#11113=ORIENTED_EDGE('',*,*,#7974,.F.);
#11114=ORIENTED_EDGE('',*,*,#7975,.F.);
#11115=ORIENTED_EDGE('',*,*,#7976,.T.);
#11116=ORIENTED_EDGE('',*,*,#7975,.T.);
#11117=ORIENTED_EDGE('',*,*,#7977,.F.);
#11118=ORIENTED_EDGE('',*,*,#7978,.F.);
#11119=ORIENTED_EDGE('',*,*,#7979,.T.);
#11120=ORIENTED_EDGE('',*,*,#7978,.T.);
#11121=ORIENTED_EDGE('',*,*,#7980,.F.);
#11122=ORIENTED_EDGE('',*,*,#7981,.F.);
#11123=ORIENTED_EDGE('',*,*,#7982,.T.);
#11124=ORIENTED_EDGE('',*,*,#7981,.T.);
#11125=ORIENTED_EDGE('',*,*,#7983,.F.);
#11126=ORIENTED_EDGE('',*,*,#7984,.F.);
#11127=ORIENTED_EDGE('',*,*,#7985,.T.);
#11128=ORIENTED_EDGE('',*,*,#7984,.T.);
#11129=ORIENTED_EDGE('',*,*,#7986,.F.);
#11130=ORIENTED_EDGE('',*,*,#7987,.F.);
#11131=ORIENTED_EDGE('',*,*,#7988,.T.);
#11132=ORIENTED_EDGE('',*,*,#7987,.T.);
#11133=ORIENTED_EDGE('',*,*,#7989,.F.);
#11134=ORIENTED_EDGE('',*,*,#7990,.F.);
#11135=ORIENTED_EDGE('',*,*,#7991,.T.);
#11136=ORIENTED_EDGE('',*,*,#7990,.T.);
#11137=ORIENTED_EDGE('',*,*,#7992,.F.);
#11138=ORIENTED_EDGE('',*,*,#7993,.F.);
#11139=ORIENTED_EDGE('',*,*,#7994,.T.);
#11140=ORIENTED_EDGE('',*,*,#7993,.T.);
#11141=ORIENTED_EDGE('',*,*,#7995,.F.);
#11142=ORIENTED_EDGE('',*,*,#7996,.F.);
#11143=ORIENTED_EDGE('',*,*,#7997,.T.);
#11144=ORIENTED_EDGE('',*,*,#7996,.T.);
#11145=ORIENTED_EDGE('',*,*,#7998,.F.);
#11146=ORIENTED_EDGE('',*,*,#7999,.F.);
#11147=ORIENTED_EDGE('',*,*,#8000,.T.);
#11148=ORIENTED_EDGE('',*,*,#7999,.T.);
#11149=ORIENTED_EDGE('',*,*,#8001,.F.);
#11150=ORIENTED_EDGE('',*,*,#7853,.F.);
#11151=ORIENTED_EDGE('',*,*,#8001,.T.);
#11152=ORIENTED_EDGE('',*,*,#7998,.T.);
#11153=ORIENTED_EDGE('',*,*,#7995,.T.);
#11154=ORIENTED_EDGE('',*,*,#7992,.T.);
#11155=ORIENTED_EDGE('',*,*,#7989,.T.);
#11156=ORIENTED_EDGE('',*,*,#7986,.T.);
#11157=ORIENTED_EDGE('',*,*,#7983,.T.);
#11158=ORIENTED_EDGE('',*,*,#7980,.T.);
#11159=ORIENTED_EDGE('',*,*,#7977,.T.);
#11160=ORIENTED_EDGE('',*,*,#7974,.T.);
#11161=ORIENTED_EDGE('',*,*,#7971,.T.);
#11162=ORIENTED_EDGE('',*,*,#7968,.T.);
#11163=ORIENTED_EDGE('',*,*,#7965,.T.);
#11164=ORIENTED_EDGE('',*,*,#7962,.T.);
#11165=ORIENTED_EDGE('',*,*,#7959,.T.);
#11166=ORIENTED_EDGE('',*,*,#7956,.T.);
#11167=ORIENTED_EDGE('',*,*,#7953,.T.);
#11168=ORIENTED_EDGE('',*,*,#7950,.T.);
#11169=ORIENTED_EDGE('',*,*,#7947,.T.);
#11170=ORIENTED_EDGE('',*,*,#7944,.T.);
#11171=ORIENTED_EDGE('',*,*,#7941,.T.);
#11172=ORIENTED_EDGE('',*,*,#7938,.T.);
#11173=ORIENTED_EDGE('',*,*,#7935,.T.);
#11174=ORIENTED_EDGE('',*,*,#7932,.T.);
#11175=ORIENTED_EDGE('',*,*,#7929,.T.);
#11176=ORIENTED_EDGE('',*,*,#7926,.T.);
#11177=ORIENTED_EDGE('',*,*,#7923,.T.);
#11178=ORIENTED_EDGE('',*,*,#7920,.T.);
#11179=ORIENTED_EDGE('',*,*,#7917,.T.);
#11180=ORIENTED_EDGE('',*,*,#7914,.T.);
#11181=ORIENTED_EDGE('',*,*,#7911,.T.);
#11182=ORIENTED_EDGE('',*,*,#7908,.T.);
#11183=ORIENTED_EDGE('',*,*,#7905,.T.);
#11184=ORIENTED_EDGE('',*,*,#7902,.T.);
#11185=ORIENTED_EDGE('',*,*,#7899,.T.);
#11186=ORIENTED_EDGE('',*,*,#7896,.T.);
#11187=ORIENTED_EDGE('',*,*,#7893,.T.);
#11188=ORIENTED_EDGE('',*,*,#7890,.T.);
#11189=ORIENTED_EDGE('',*,*,#7887,.T.);
#11190=ORIENTED_EDGE('',*,*,#7884,.T.);
#11191=ORIENTED_EDGE('',*,*,#7881,.T.);
#11192=ORIENTED_EDGE('',*,*,#7878,.T.);
#11193=ORIENTED_EDGE('',*,*,#7875,.T.);
#11194=ORIENTED_EDGE('',*,*,#7872,.T.);
#11195=ORIENTED_EDGE('',*,*,#7869,.T.);
#11196=ORIENTED_EDGE('',*,*,#7866,.T.);
#11197=ORIENTED_EDGE('',*,*,#7863,.T.);
#11198=ORIENTED_EDGE('',*,*,#7860,.T.);
#11199=ORIENTED_EDGE('',*,*,#7857,.T.);
#11200=ORIENTED_EDGE('',*,*,#7854,.T.);
#11201=ORIENTED_EDGE('',*,*,#8000,.F.);
#11202=ORIENTED_EDGE('',*,*,#7852,.F.);
#11203=ORIENTED_EDGE('',*,*,#7856,.F.);
#11204=ORIENTED_EDGE('',*,*,#7859,.F.);
#11205=ORIENTED_EDGE('',*,*,#7862,.F.);
#11206=ORIENTED_EDGE('',*,*,#7865,.F.);
#11207=ORIENTED_EDGE('',*,*,#7868,.F.);
#11208=ORIENTED_EDGE('',*,*,#7871,.F.);
#11209=ORIENTED_EDGE('',*,*,#7874,.F.);
#11210=ORIENTED_EDGE('',*,*,#7877,.F.);
#11211=ORIENTED_EDGE('',*,*,#7880,.F.);
#11212=ORIENTED_EDGE('',*,*,#7883,.F.);
#11213=ORIENTED_EDGE('',*,*,#7886,.F.);
#11214=ORIENTED_EDGE('',*,*,#7889,.F.);
#11215=ORIENTED_EDGE('',*,*,#7892,.F.);
#11216=ORIENTED_EDGE('',*,*,#7895,.F.);
#11217=ORIENTED_EDGE('',*,*,#7898,.F.);
#11218=ORIENTED_EDGE('',*,*,#7901,.F.);
#11219=ORIENTED_EDGE('',*,*,#7904,.F.);
#11220=ORIENTED_EDGE('',*,*,#7907,.F.);
#11221=ORIENTED_EDGE('',*,*,#7910,.F.);
#11222=ORIENTED_EDGE('',*,*,#7913,.F.);
#11223=ORIENTED_EDGE('',*,*,#7916,.F.);
#11224=ORIENTED_EDGE('',*,*,#7919,.F.);
#11225=ORIENTED_EDGE('',*,*,#7922,.F.);
#11226=ORIENTED_EDGE('',*,*,#7925,.F.);
#11227=ORIENTED_EDGE('',*,*,#7928,.F.);
#11228=ORIENTED_EDGE('',*,*,#7931,.F.);
#11229=ORIENTED_EDGE('',*,*,#7934,.F.);
#11230=ORIENTED_EDGE('',*,*,#7937,.F.);
#11231=ORIENTED_EDGE('',*,*,#7940,.F.);
#11232=ORIENTED_EDGE('',*,*,#7943,.F.);
#11233=ORIENTED_EDGE('',*,*,#7946,.F.);
#11234=ORIENTED_EDGE('',*,*,#7949,.F.);
#11235=ORIENTED_EDGE('',*,*,#7952,.F.);
#11236=ORIENTED_EDGE('',*,*,#7955,.F.);
#11237=ORIENTED_EDGE('',*,*,#7958,.F.);
#11238=ORIENTED_EDGE('',*,*,#7961,.F.);
#11239=ORIENTED_EDGE('',*,*,#7964,.F.);
#11240=ORIENTED_EDGE('',*,*,#7967,.F.);
#11241=ORIENTED_EDGE('',*,*,#7970,.F.);
#11242=ORIENTED_EDGE('',*,*,#7973,.F.);
#11243=ORIENTED_EDGE('',*,*,#7976,.F.);
#11244=ORIENTED_EDGE('',*,*,#7979,.F.);
#11245=ORIENTED_EDGE('',*,*,#7982,.F.);
#11246=ORIENTED_EDGE('',*,*,#7985,.F.);
#11247=ORIENTED_EDGE('',*,*,#7988,.F.);
#11248=ORIENTED_EDGE('',*,*,#7991,.F.);
#11249=ORIENTED_EDGE('',*,*,#7994,.F.);
#11250=ORIENTED_EDGE('',*,*,#7997,.F.);
#12798=PLANE('',#14638);
#12799=PLANE('',#14639);
#12800=PLANE('',#14640);
#12801=PLANE('',#14641);
#12802=PLANE('',#14642);
#12803=PLANE('',#14643);
#12804=PLANE('',#14644);
#12805=PLANE('',#14645);
#12806=PLANE('',#14646);
#12807=PLANE('',#14647);
#12808=PLANE('',#14648);
#12809=PLANE('',#14649);
#12810=PLANE('',#14650);
#12811=PLANE('',#14651);
#12812=PLANE('',#14652);
#12813=PLANE('',#14653);
#12814=PLANE('',#14654);
#12815=PLANE('',#14655);
#12816=PLANE('',#14656);
#12817=PLANE('',#14657);
#12818=PLANE('',#14658);
#12819=PLANE('',#14659);
#12820=PLANE('',#14660);
#12821=PLANE('',#14661);
#12822=PLANE('',#14662);
#12823=PLANE('',#14663);
#12824=PLANE('',#14664);
#12825=PLANE('',#14665);
#12826=PLANE('',#14666);
#12827=PLANE('',#14667);
#12828=PLANE('',#14668);
#12829=PLANE('',#14669);
#12830=PLANE('',#14670);
#12831=PLANE('',#14671);
#12832=PLANE('',#14672);
#12833=PLANE('',#14673);
#12834=PLANE('',#14674);
#12835=PLANE('',#14675);
#12836=PLANE('',#14676);
#12837=PLANE('',#14677);
#12838=PLANE('',#14678);
#12839=PLANE('',#14679);
#12840=PLANE('',#14680);
#12841=PLANE('',#14681);
#12842=PLANE('',#14682);
#12843=PLANE('',#14683);
#12844=PLANE('',#14684);
#12845=PLANE('',#14685);
#12846=PLANE('',#14686);
#12847=PLANE('',#14687);
#12848=PLANE('',#14688);
#12849=PLANE('',#14689);
#13486=ADVANCED_FACE('',(#1723),#12798,.T.);
#13487=ADVANCED_FACE('',(#1724),#12799,.T.);
#13488=ADVANCED_FACE('',(#1725),#12800,.T.);
#13489=ADVANCED_FACE('',(#1726),#12801,.T.);
#13490=ADVANCED_FACE('',(#1727),#12802,.T.);
#13491=ADVANCED_FACE('',(#1728),#12803,.T.);
#13492=ADVANCED_FACE('',(#1729),#12804,.T.);
#13493=ADVANCED_FACE('',(#1730),#12805,.T.);
#13494=ADVANCED_FACE('',(#1731),#12806,.T.);
#13495=ADVANCED_FACE('',(#1732),#12807,.T.);
#13496=ADVANCED_FACE('',(#1733),#12808,.T.);
#13497=ADVANCED_FACE('',(#1734),#12809,.T.);
#13498=ADVANCED_FACE('',(#1735),#12810,.T.);
#13499=ADVANCED_FACE('',(#1736),#12811,.T.);
#13500=ADVANCED_FACE('',(#1737),#12812,.T.);
#13501=ADVANCED_FACE('',(#1738),#12813,.T.);
#13502=ADVANCED_FACE('',(#1739),#12814,.T.);
#13503=ADVANCED_FACE('',(#1740),#12815,.T.);
#13504=ADVANCED_FACE('',(#1741),#12816,.T.);
#13505=ADVANCED_FACE('',(#1742),#12817,.T.);
#13506=ADVANCED_FACE('',(#1743),#12818,.T.);
#13507=ADVANCED_FACE('',(#1744),#12819,.T.);
#13508=ADVANCED_FACE('',(#1745),#12820,.T.);
#13509=ADVANCED_FACE('',(#1746),#12821,.T.);
#13510=ADVANCED_FACE('',(#1747),#12822,.T.);
#13511=ADVANCED_FACE('',(#1748),#12823,.T.);
#13512=ADVANCED_FACE('',(#1749),#12824,.T.);
#13513=ADVANCED_FACE('',(#1750),#12825,.T.);
#13514=ADVANCED_FACE('',(#1751),#12826,.T.);
#13515=ADVANCED_FACE('',(#1752),#12827,.T.);
#13516=ADVANCED_FACE('',(#1753),#12828,.T.);
#13517=ADVANCED_FACE('',(#1754),#12829,.T.);
#13518=ADVANCED_FACE('',(#1755),#12830,.T.);
#13519=ADVANCED_FACE('',(#1756),#12831,.T.);
#13520=ADVANCED_FACE('',(#1757),#12832,.T.);
#13521=ADVANCED_FACE('',(#1758),#12833,.T.);
#13522=ADVANCED_FACE('',(#1759),#12834,.T.);
#13523=ADVANCED_FACE('',(#1760),#12835,.T.);
#13524=ADVANCED_FACE('',(#1761),#12836,.T.);
#13525=ADVANCED_FACE('',(#1762),#12837,.T.);
#13526=ADVANCED_FACE('',(#1763),#12838,.T.);
#13527=ADVANCED_FACE('',(#1764),#12839,.T.);
#13528=ADVANCED_FACE('',(#1765),#12840,.T.);
#13529=ADVANCED_FACE('',(#1766),#12841,.T.);
#13530=ADVANCED_FACE('',(#1767),#12842,.T.);
#13531=ADVANCED_FACE('',(#1768),#12843,.T.);
#13532=ADVANCED_FACE('',(#1769),#12844,.T.);
#13533=ADVANCED_FACE('',(#1770),#12845,.T.);
#13534=ADVANCED_FACE('',(#1771),#12846,.T.);
#13535=ADVANCED_FACE('',(#1772),#12847,.T.);
#13536=ADVANCED_FACE('',(#1773),#12848,.T.);
#13537=ADVANCED_FACE('',(#1774),#12849,.F.);
#13814=CLOSED_SHELL('',(#13486,#13487,#13488,#13489,#13490,#13491,#13492,
#13493,#13494,#13495,#13496,#13497,#13498,#13499,#13500,#13501,#13502,#13503,
#13504,#13505,#13506,#13507,#13508,#13509,#13510,#13511,#13512,#13513,#13514,
#13515,#13516,#13517,#13518,#13519,#13520,#13521,#13522,#13523,#13524,#13525,
#13526,#13527,#13528,#13529,#13530,#13531,#13532,#13533,#13534,#13535,#13536,
#13537));
#14637=AXIS2_PLACEMENT_3D('',#26541,#17004,#17005);
#14638=AXIS2_PLACEMENT_3D('',#26542,#17006,#17007);
#14639=AXIS2_PLACEMENT_3D('',#26551,#17012,#17013);
#14640=AXIS2_PLACEMENT_3D('',#26557,#17017,#17018);
#14641=AXIS2_PLACEMENT_3D('',#26563,#17022,#17023);
#14642=AXIS2_PLACEMENT_3D('',#26569,#17027,#17028);
#14643=AXIS2_PLACEMENT_3D('',#26575,#17032,#17033);
#14644=AXIS2_PLACEMENT_3D('',#26581,#17037,#17038);
#14645=AXIS2_PLACEMENT_3D('',#26587,#17042,#17043);
#14646=AXIS2_PLACEMENT_3D('',#26593,#17047,#17048);
#14647=AXIS2_PLACEMENT_3D('',#26599,#17052,#17053);
#14648=AXIS2_PLACEMENT_3D('',#26605,#17057,#17058);
#14649=AXIS2_PLACEMENT_3D('',#26611,#17062,#17063);
#14650=AXIS2_PLACEMENT_3D('',#26617,#17067,#17068);
#14651=AXIS2_PLACEMENT_3D('',#26623,#17072,#17073);
#14652=AXIS2_PLACEMENT_3D('',#26629,#17077,#17078);
#14653=AXIS2_PLACEMENT_3D('',#26635,#17082,#17083);
#14654=AXIS2_PLACEMENT_3D('',#26641,#17087,#17088);
#14655=AXIS2_PLACEMENT_3D('',#26647,#17092,#17093);
#14656=AXIS2_PLACEMENT_3D('',#26653,#17097,#17098);
#14657=AXIS2_PLACEMENT_3D('',#26659,#17102,#17103);
#14658=AXIS2_PLACEMENT_3D('',#26665,#17107,#17108);
#14659=AXIS2_PLACEMENT_3D('',#26671,#17112,#17113);
#14660=AXIS2_PLACEMENT_3D('',#26677,#17117,#17118);
#14661=AXIS2_PLACEMENT_3D('',#26683,#17122,#17123);
#14662=AXIS2_PLACEMENT_3D('',#26689,#17127,#17128);
#14663=AXIS2_PLACEMENT_3D('',#26695,#17132,#17133);
#14664=AXIS2_PLACEMENT_3D('',#26701,#17137,#17138);
#14665=AXIS2_PLACEMENT_3D('',#26707,#17142,#17143);
#14666=AXIS2_PLACEMENT_3D('',#26713,#17147,#17148);
#14667=AXIS2_PLACEMENT_3D('',#26719,#17152,#17153);
#14668=AXIS2_PLACEMENT_3D('',#26725,#17157,#17158);
#14669=AXIS2_PLACEMENT_3D('',#26731,#17162,#17163);
#14670=AXIS2_PLACEMENT_3D('',#26737,#17167,#17168);
#14671=AXIS2_PLACEMENT_3D('',#26743,#17172,#17173);
#14672=AXIS2_PLACEMENT_3D('',#26749,#17177,#17178);
#14673=AXIS2_PLACEMENT_3D('',#26755,#17182,#17183);
#14674=AXIS2_PLACEMENT_3D('',#26761,#17187,#17188);
#14675=AXIS2_PLACEMENT_3D('',#26767,#17192,#17193);
#14676=AXIS2_PLACEMENT_3D('',#26773,#17197,#17198);
#14677=AXIS2_PLACEMENT_3D('',#26779,#17202,#17203);
#14678=AXIS2_PLACEMENT_3D('',#26785,#17207,#17208);
#14679=AXIS2_PLACEMENT_3D('',#26791,#17212,#17213);
#14680=AXIS2_PLACEMENT_3D('',#26797,#17217,#17218);
#14681=AXIS2_PLACEMENT_3D('',#26803,#17222,#17223);
#14682=AXIS2_PLACEMENT_3D('',#26809,#17227,#17228);
#14683=AXIS2_PLACEMENT_3D('',#26815,#17232,#17233);
#14684=AXIS2_PLACEMENT_3D('',#26821,#17237,#17238);
#14685=AXIS2_PLACEMENT_3D('',#26827,#17242,#17243);
#14686=AXIS2_PLACEMENT_3D('',#26833,#17247,#17248);
#14687=AXIS2_PLACEMENT_3D('',#26839,#17252,#17253);
#14688=AXIS2_PLACEMENT_3D('',#26842,#17256,#17257);
#14689=AXIS2_PLACEMENT_3D('',#26843,#17258,#17259);
#17004=DIRECTION('axis',(0.,0.,1.));
#17005=DIRECTION('refdir',(1.,0.,0.));
#17006=DIRECTION('center_axis',(0.,-0.934100663920609,-0.357009733288993));
#17007=DIRECTION('ref_axis',(0.,0.357009733288993,-0.934100663920609));
#17008=DIRECTION('',(0.,0.357009733288993,-0.934100663920609));
#17009=DIRECTION('',(1.,0.,0.));
#17010=DIRECTION('',(0.,0.357009733288993,-0.934100663920609));
#17011=DIRECTION('',(1.,0.,0.));
#17012=DIRECTION('center_axis',(0.,-0.821646937942163,-0.569996762596303));
#17013=DIRECTION('ref_axis',(0.,0.569996762596303,-0.821646937942163));
#17014=DIRECTION('',(0.,0.569996762596303,-0.821646937942163));
#17015=DIRECTION('',(0.,0.569996762596303,-0.821646937942163));
#17016=DIRECTION('',(1.,0.,0.));
#17017=DIRECTION('center_axis',(0.,-0.661530035807154,-0.749918670073619));
#17018=DIRECTION('ref_axis',(0.,0.749918670073619,-0.661530035807154));
#17019=DIRECTION('',(0.,0.749918670073619,-0.661530035807154));
#17020=DIRECTION('',(0.,0.749918670073619,-0.661530035807154));
#17021=DIRECTION('',(1.,0.,0.));
#17022=DIRECTION('center_axis',(0.,-0.463038229350705,-0.886338309089573));
#17023=DIRECTION('ref_axis',(0.,0.886338309089573,-0.463038229350705));
#17024=DIRECTION('',(0.,0.886338309089573,-0.463038229350705));
#17025=DIRECTION('',(0.,0.886338309089573,-0.463038229350705));
#17026=DIRECTION('',(1.,0.,0.));
#17027=DIRECTION('center_axis',(0.,-0.237685892326173,-0.971342069813262));
#17028=DIRECTION('ref_axis',(0.,0.971342069813261,-0.237685892326173));
#17029=DIRECTION('',(0.,0.971342069813261,-0.237685892326173));
#17030=DIRECTION('',(0.,0.971342069813261,-0.237685892326173));
#17031=DIRECTION('',(1.,0.,0.));
#17032=DIRECTION('center_axis',(0.,0.00145444053054168,-0.999998942300812));
#17033=DIRECTION('ref_axis',(0.,0.999998942300812,0.00145444053054168));
#17034=DIRECTION('',(0.,0.999998942300812,0.00145444053054168));
#17035=DIRECTION('',(0.,0.999998942300812,0.00145444053054168));
#17036=DIRECTION('',(1.,0.,0.));
#17037=DIRECTION('center_axis',(0.,0.240510402288168,-0.970646561005181));
#17038=DIRECTION('ref_axis',(0.,0.97064656100518,0.240510402288168));
#17039=DIRECTION('',(0.,0.97064656100518,0.240510402288168));
#17040=DIRECTION('',(0.,0.97064656100518,0.240510402288168));
#17041=DIRECTION('',(1.,0.,0.));
#17042=DIRECTION('center_axis',(0.,0.465614520325111,-0.884987637463042));
#17043=DIRECTION('ref_axis',(0.,0.884987637463042,0.465614520325111));
#17044=DIRECTION('',(0.,0.884987637463042,0.465614520325111));
#17045=DIRECTION('',(0.,0.884987637463042,0.465614520325111));
#17046=DIRECTION('',(1.,0.,0.));
#17047=DIRECTION('center_axis',(0.,0.663708658918947,-0.74799118716467));
#17048=DIRECTION('ref_axis',(0.,0.74799118716467,0.663708658918947));
#17049=DIRECTION('',(0.,0.74799118716467,0.663708658918947));
#17050=DIRECTION('',(0.,0.74799118716467,0.663708658918947));
#17051=DIRECTION('',(1.,0.,0.));
#17052=DIRECTION('center_axis',(0.,0.82330151275668,-0.567604280368428));
#17053=DIRECTION('ref_axis',(0.,0.567604280368429,0.823301512756681));
#17054=DIRECTION('',(0.,0.567604280368428,0.82330151275668));
#17055=DIRECTION('',(0.,0.567604280368428,0.82330151275668));
#17056=DIRECTION('',(1.,0.,0.));
#17057=DIRECTION('center_axis',(0.,0.935135209686012,-0.354291037997716));
#17058=DIRECTION('ref_axis',(0.,0.354291037997716,0.935135209686012));
#17059=DIRECTION('',(0.,0.354291037997716,0.935135209686012));
#17060=DIRECTION('',(0.,0.354291037997716,0.935135209686012));
#17061=DIRECTION('',(1.,0.,0.));
#17062=DIRECTION('center_axis',(0.,0.992722353538543,-0.120425615152662));
#17063=DIRECTION('ref_axis',(0.,0.120425615152662,0.992722353538542));
#17064=DIRECTION('',(0.,0.120425615152662,0.992722353538542));
#17065=DIRECTION('',(0.,0.120425615152662,0.992722353538542));
#17066=DIRECTION('',(1.,0.,0.));
#17067=DIRECTION('center_axis',(0.,0.992722353538543,0.120425615152661));
#17068=DIRECTION('ref_axis',(0.,-0.120425615152661,0.992722353538543));
#17069=DIRECTION('',(0.,-0.120425615152661,0.992722353538543));
#17070=DIRECTION('',(0.,-0.120425615152661,0.992722353538543));
#17071=DIRECTION('',(1.,0.,0.));
#17072=DIRECTION('center_axis',(0.,0.935135209686012,0.354291037997715));
#17073=DIRECTION('ref_axis',(0.,-0.354291037997715,0.935135209686012));
#17074=DIRECTION('',(0.,-0.354291037997715,0.935135209686012));
#17075=DIRECTION('',(0.,-0.354291037997715,0.935135209686012));
#17076=DIRECTION('',(1.,0.,0.));
#17077=DIRECTION('center_axis',(0.,0.82330151275668,0.567604280368429));
#17078=DIRECTION('ref_axis',(0.,-0.567604280368429,0.82330151275668));
#17079=DIRECTION('',(0.,-0.567604280368429,0.82330151275668));
#17080=DIRECTION('',(0.,-0.567604280368429,0.82330151275668));
#17081=DIRECTION('',(1.,0.,0.));
#17082=DIRECTION('center_axis',(0.,0.663708658918947,0.747991187164671));
#17083=DIRECTION('ref_axis',(0.,-0.747991187164671,0.663708658918947));
#17084=DIRECTION('',(0.,-0.747991187164671,0.663708658918946));
#17085=DIRECTION('',(0.,-0.747991187164671,0.663708658918946));
#17086=DIRECTION('',(1.,0.,0.));
#17087=DIRECTION('center_axis',(0.,0.465614520325111,0.884987637463042));
#17088=DIRECTION('ref_axis',(0.,-0.884987637463042,0.465614520325111));
#17089=DIRECTION('',(0.,-0.884987637463042,0.465614520325111));
#17090=DIRECTION('',(0.,-0.884987637463042,0.465614520325111));
#17091=DIRECTION('',(1.,0.,0.));
#17092=DIRECTION('center_axis',(0.,0.240510402288168,0.97064656100518));
#17093=DIRECTION('ref_axis',(0.,-0.97064656100518,0.240510402288168));
#17094=DIRECTION('',(0.,-0.97064656100518,0.240510402288168));
#17095=DIRECTION('',(0.,-0.97064656100518,0.240510402288168));
#17096=DIRECTION('',(1.,0.,0.));
#17097=DIRECTION('center_axis',(0.,0.00145444053054169,0.999998942300812));
#17098=DIRECTION('ref_axis',(0.,-0.999998942300812,0.00145444053054169));
#17099=DIRECTION('',(0.,-0.999998942300812,0.00145444053054169));
#17100=DIRECTION('',(0.,-0.999998942300812,0.00145444053054169));
#17101=DIRECTION('',(1.,0.,0.));
#17102=DIRECTION('center_axis',(0.,-0.237685892326173,0.971342069813261));
#17103=DIRECTION('ref_axis',(0.,-0.971342069813261,-0.237685892326173));
#17104=DIRECTION('',(0.,-0.971342069813261,-0.237685892326173));
#17105=DIRECTION('',(0.,-0.971342069813261,-0.237685892326173));
#17106=DIRECTION('',(1.,0.,0.));
#17107=DIRECTION('center_axis',(0.,-0.463038229350704,0.886338309089574));
#17108=DIRECTION('ref_axis',(0.,-0.886338309089573,-0.463038229350704));
#17109=DIRECTION('',(0.,-0.886338309089573,-0.463038229350704));
#17110=DIRECTION('',(0.,-0.886338309089573,-0.463038229350704));
#17111=DIRECTION('',(1.,0.,0.));
#17112=DIRECTION('center_axis',(0.,-0.661530035807154,0.749918670073619));
#17113=DIRECTION('ref_axis',(0.,-0.749918670073619,-0.661530035807154));
#17114=DIRECTION('',(0.,-0.749918670073619,-0.661530035807154));
#17115=DIRECTION('',(0.,-0.749918670073619,-0.661530035807154));
#17116=DIRECTION('',(1.,0.,0.));
#17117=DIRECTION('center_axis',(0.,-0.821646937942163,0.569996762596303));
#17118=DIRECTION('ref_axis',(0.,-0.569996762596303,-0.821646937942163));
#17119=DIRECTION('',(0.,-0.569996762596303,-0.821646937942163));
#17120=DIRECTION('',(0.,-0.569996762596303,-0.821646937942163));
#17121=DIRECTION('',(1.,0.,0.));
#17122=DIRECTION('center_axis',(0.,-0.934100663920608,0.357009733288994));
#17123=DIRECTION('ref_axis',(0.,-0.357009733288994,-0.934100663920608));
#17124=DIRECTION('',(0.,-0.357009733288994,-0.934100663920608));
#17125=DIRECTION('',(0.,-0.357009733288994,-0.934100663920608));
#17126=DIRECTION('',(1.,0.,0.));
#17127=DIRECTION('center_axis',(0.,0.241921895599669,0.970295726275996));
#17128=DIRECTION('ref_axis',(0.,-0.970295726275996,0.241921895599669));
#17129=DIRECTION('',(0.,-0.970295726275996,0.241921895599669));
#17130=DIRECTION('',(0.,-0.970295726275996,0.241921895599669));
#17131=DIRECTION('',(1.,0.,0.));
#17132=DIRECTION('center_axis',(0.,0.934100663920609,-0.357009733288994));
#17133=DIRECTION('ref_axis',(0.,0.357009733288994,0.934100663920609));
#17134=DIRECTION('',(0.,0.357009733288994,0.934100663920608));
#17135=DIRECTION('',(0.,0.357009733288994,0.934100663920608));
#17136=DIRECTION('',(1.,0.,0.));
#17137=DIRECTION('center_axis',(0.,0.821646937942163,-0.569996762596304));
#17138=DIRECTION('ref_axis',(0.,0.569996762596304,0.821646937942163));
#17139=DIRECTION('',(0.,0.569996762596304,0.821646937942163));
#17140=DIRECTION('',(0.,0.569996762596304,0.821646937942163));
#17141=DIRECTION('',(1.,0.,0.));
#17142=DIRECTION('center_axis',(0.,0.661530035807154,-0.749918670073619));
#17143=DIRECTION('ref_axis',(0.,0.749918670073619,0.661530035807154));
#17144=DIRECTION('',(0.,0.749918670073619,0.661530035807154));
#17145=DIRECTION('',(0.,0.749918670073619,0.661530035807154));
#17146=DIRECTION('',(1.,0.,0.));
#17147=DIRECTION('center_axis',(0.,0.463038229350705,-0.886338309089573));
#17148=DIRECTION('ref_axis',(0.,0.886338309089573,0.463038229350705));
#17149=DIRECTION('',(0.,0.886338309089573,0.463038229350705));
#17150=DIRECTION('',(0.,0.886338309089573,0.463038229350705));
#17151=DIRECTION('',(1.,0.,0.));
#17152=DIRECTION('center_axis',(0.,0.237685892326173,-0.971342069813261));
#17153=DIRECTION('ref_axis',(0.,0.971342069813261,0.237685892326173));
#17154=DIRECTION('',(0.,0.971342069813261,0.237685892326173));
#17155=DIRECTION('',(0.,0.971342069813261,0.237685892326173));
#17156=DIRECTION('',(1.,0.,0.));
#17157=DIRECTION('center_axis',(0.,-0.00145444053054132,-0.999998942300812));
#17158=DIRECTION('ref_axis',(0.,0.999998942300812,-0.00145444053054132));
#17159=DIRECTION('',(0.,0.999998942300812,-0.00145444053054132));
#17160=DIRECTION('',(0.,0.999998942300812,-0.00145444053054132));
#17161=DIRECTION('',(1.,0.,0.));
#17162=DIRECTION('center_axis',(0.,-0.240510402288168,-0.97064656100518));
#17163=DIRECTION('ref_axis',(0.,0.97064656100518,-0.240510402288168));
#17164=DIRECTION('',(0.,0.97064656100518,-0.240510402288168));
#17165=DIRECTION('',(0.,0.97064656100518,-0.240510402288168));
#17166=DIRECTION('',(1.,0.,0.));
#17167=DIRECTION('center_axis',(0.,-0.465614520325111,-0.884987637463042));
#17168=DIRECTION('ref_axis',(0.,0.884987637463042,-0.465614520325111));
#17169=DIRECTION('',(0.,0.884987637463042,-0.465614520325111));
#17170=DIRECTION('',(0.,0.884987637463042,-0.465614520325111));
#17171=DIRECTION('',(1.,0.,0.));
#17172=DIRECTION('center_axis',(0.,-0.663708658918947,-0.74799118716467));
#17173=DIRECTION('ref_axis',(0.,0.74799118716467,-0.663708658918947));
#17174=DIRECTION('',(0.,0.74799118716467,-0.663708658918947));
#17175=DIRECTION('',(0.,0.74799118716467,-0.663708658918947));
#17176=DIRECTION('',(1.,0.,0.));
#17177=DIRECTION('center_axis',(0.,-0.82330151275668,-0.567604280368429));
#17178=DIRECTION('ref_axis',(0.,0.567604280368429,-0.82330151275668));
#17179=DIRECTION('',(0.,0.567604280368429,-0.82330151275668));
#17180=DIRECTION('',(0.,0.567604280368429,-0.82330151275668));
#17181=DIRECTION('',(1.,0.,0.));
#17182=DIRECTION('center_axis',(0.,-0.935135209686012,-0.354291037997715));
#17183=DIRECTION('ref_axis',(0.,0.354291037997715,-0.935135209686012));
#17184=DIRECTION('',(0.,0.354291037997715,-0.935135209686012));
#17185=DIRECTION('',(0.,0.354291037997715,-0.935135209686012));
#17186=DIRECTION('',(1.,0.,0.));
#17187=DIRECTION('center_axis',(0.,-0.992722353538543,-0.120425615152661));
#17188=DIRECTION('ref_axis',(0.,0.120425615152661,-0.992722353538542));
#17189=DIRECTION('',(0.,0.120425615152661,-0.992722353538543));
#17190=DIRECTION('',(0.,0.120425615152661,-0.992722353538543));
#17191=DIRECTION('',(1.,0.,0.));
#17192=DIRECTION('center_axis',(0.,-0.992722353538543,0.120425615152662));
#17193=DIRECTION('ref_axis',(0.,-0.120425615152662,-0.992722353538542));
#17194=DIRECTION('',(0.,-0.120425615152662,-0.992722353538542));
#17195=DIRECTION('',(0.,-0.120425615152662,-0.992722353538542));
#17196=DIRECTION('',(1.,0.,0.));
#17197=DIRECTION('center_axis',(0.,-0.935135209686012,0.354291037997716));
#17198=DIRECTION('ref_axis',(0.,-0.354291037997716,-0.935135209686012));
#17199=DIRECTION('',(0.,-0.354291037997716,-0.935135209686012));
#17200=DIRECTION('',(0.,-0.354291037997716,-0.935135209686012));
#17201=DIRECTION('',(1.,0.,0.));
#17202=DIRECTION('center_axis',(0.,-0.82330151275668,0.567604280368429));
#17203=DIRECTION('ref_axis',(0.,-0.567604280368429,-0.82330151275668));
#17204=DIRECTION('',(0.,-0.567604280368429,-0.82330151275668));
#17205=DIRECTION('',(0.,-0.567604280368429,-0.82330151275668));
#17206=DIRECTION('',(1.,0.,0.));
#17207=DIRECTION('center_axis',(0.,-0.663708658918947,0.74799118716467));
#17208=DIRECTION('ref_axis',(0.,-0.74799118716467,-0.663708658918947));
#17209=DIRECTION('',(0.,-0.74799118716467,-0.663708658918947));
#17210=DIRECTION('',(0.,-0.74799118716467,-0.663708658918947));
#17211=DIRECTION('',(1.,0.,0.));
#17212=DIRECTION('center_axis',(0.,-0.465614520325111,0.884987637463042));
#17213=DIRECTION('ref_axis',(0.,-0.884987637463042,-0.465614520325111));
#17214=DIRECTION('',(0.,-0.884987637463042,-0.465614520325111));
#17215=DIRECTION('',(0.,-0.884987637463042,-0.465614520325111));
#17216=DIRECTION('',(1.,0.,0.));
#17217=DIRECTION('center_axis',(0.,-0.240510402288169,0.97064656100518));
#17218=DIRECTION('ref_axis',(0.,-0.97064656100518,-0.240510402288169));
#17219=DIRECTION('',(0.,-0.97064656100518,-0.240510402288169));
#17220=DIRECTION('',(0.,-0.97064656100518,-0.240510402288169));
#17221=DIRECTION('',(1.,0.,0.));
#17222=DIRECTION('center_axis',(0.,-0.00145444053054131,0.999998942300812));
#17223=DIRECTION('ref_axis',(0.,-0.999998942300812,-0.00145444053054131));
#17224=DIRECTION('',(0.,-0.999998942300812,-0.00145444053054131));
#17225=DIRECTION('',(0.,-0.999998942300812,-0.00145444053054131));
#17226=DIRECTION('',(1.,0.,0.));
#17227=DIRECTION('center_axis',(0.,0.237685892326173,0.971342069813262));
#17228=DIRECTION('ref_axis',(0.,-0.971342069813262,0.237685892326173));
#17229=DIRECTION('',(0.,-0.971342069813262,0.237685892326173));
#17230=DIRECTION('',(0.,-0.971342069813262,0.237685892326173));
#17231=DIRECTION('',(1.,0.,0.));
#17232=DIRECTION('center_axis',(0.,0.463038229350705,0.886338309089573));
#17233=DIRECTION('ref_axis',(0.,-0.886338309089573,0.463038229350705));
#17234=DIRECTION('',(0.,-0.886338309089573,0.463038229350705));
#17235=DIRECTION('',(0.,-0.886338309089573,0.463038229350705));
#17236=DIRECTION('',(1.,0.,0.));
#17237=DIRECTION('center_axis',(0.,0.661530035807154,0.749918670073619));
#17238=DIRECTION('ref_axis',(0.,-0.749918670073619,0.661530035807154));
#17239=DIRECTION('',(0.,-0.749918670073619,0.661530035807154));
#17240=DIRECTION('',(0.,-0.749918670073619,0.661530035807154));
#17241=DIRECTION('',(1.,0.,0.));
#17242=DIRECTION('center_axis',(0.,0.821646937942164,0.569996762596303));
#17243=DIRECTION('ref_axis',(0.,-0.569996762596303,0.821646937942164));
#17244=DIRECTION('',(0.,-0.569996762596303,0.821646937942164));
#17245=DIRECTION('',(0.,-0.569996762596303,0.821646937942164));
#17246=DIRECTION('',(1.,0.,0.));
#17247=DIRECTION('center_axis',(0.,0.934100663920609,0.357009733288993));
#17248=DIRECTION('ref_axis',(0.,-0.357009733288993,0.934100663920609));
#17249=DIRECTION('',(0.,-0.357009733288993,0.934100663920609));
#17250=DIRECTION('',(0.,-0.357009733288993,0.934100663920609));
#17251=DIRECTION('',(1.,0.,0.));
#17252=DIRECTION('center_axis',(0.,0.241921895599668,-0.970295726275996));
#17253=DIRECTION('ref_axis',(0.,0.970295726275996,0.241921895599668));
#17254=DIRECTION('',(0.,0.970295726275996,0.241921895599668));
#17255=DIRECTION('',(0.,0.970295726275996,0.241921895599668));
#17256=DIRECTION('center_axis',(1.,0.,0.));
#17257=DIRECTION('ref_axis',(0.,0.,-1.));
#17258=DIRECTION('center_axis',(1.,0.,0.));
#17259=DIRECTION('ref_axis',(0.,0.,-1.));
#26541=CARTESIAN_POINT('',(0.,0.,0.));
#26542=CARTESIAN_POINT('Origin',(0.,1.57407089715261,0.831084117726459));
#26543=CARTESIAN_POINT('',(0.,1.57407089715261,0.831084117726459));
#26544=CARTESIAN_POINT('',(0.,1.72712639277127,0.430620974167409));
#26545=CARTESIAN_POINT('',(0.,1.57407089715261,0.831084117726459));
#26546=CARTESIAN_POINT('',(12.,1.72712639277127,0.430620974167409));
#26547=CARTESIAN_POINT('',(0.,1.72712639277127,0.430620974167409));
#26548=CARTESIAN_POINT('',(12.,1.57407089715261,0.831084117726459));
#26549=CARTESIAN_POINT('',(12.,1.57407089715261,0.831084117726459));
#26550=CARTESIAN_POINT('',(0.,1.57407089715261,0.831084117726459));
#26551=CARTESIAN_POINT('Origin',(0.,1.32970462680897,1.18333664079281));
#26552=CARTESIAN_POINT('',(0.,1.32970462680897,1.18333664079281));
#26553=CARTESIAN_POINT('',(0.,1.32970462680897,1.18333664079281));
#26554=CARTESIAN_POINT('',(12.,1.32970462680897,1.18333664079281));
#26555=CARTESIAN_POINT('',(12.,1.32970462680897,1.18333664079281));
#26556=CARTESIAN_POINT('',(0.,1.32970462680897,1.18333664079281));
#26557=CARTESIAN_POINT('Origin',(0.,1.0082031017262,1.46694461574719));
#26558=CARTESIAN_POINT('',(0.,1.0082031017262,1.46694461574719));
#26559=CARTESIAN_POINT('',(0.,1.0082031017262,1.46694461574719));
#26560=CARTESIAN_POINT('',(12.,1.0082031017262,1.46694461574719));
#26561=CARTESIAN_POINT('',(12.,1.0082031017262,1.46694461574719));
#26562=CARTESIAN_POINT('',(0.,1.0082031017262,1.46694461574719));
#26563=CARTESIAN_POINT('Origin',(0.,0.628216405190687,1.66545613819437));
#26564=CARTESIAN_POINT('',(0.,0.628216405190687,1.66545613819437));
#26565=CARTESIAN_POINT('',(0.,0.628216405190687,1.66545613819437));
#26566=CARTESIAN_POINT('',(12.,0.628216405190687,1.66545613819437));
#26567=CARTESIAN_POINT('',(12.,0.628216405190687,1.66545613819437));
#26568=CARTESIAN_POINT('',(0.,0.628216405190687,1.66545613819437));
#26569=CARTESIAN_POINT('Origin',(0.,0.211787305230605,1.76735569066987));
#26570=CARTESIAN_POINT('',(0.,0.211787305230605,1.76735569066987));
#26571=CARTESIAN_POINT('',(0.,0.211787305230605,1.76735569066987));
#26572=CARTESIAN_POINT('',(12.,0.211787305230605,1.76735569066987));
#26573=CARTESIAN_POINT('',(12.,0.211787305230605,1.76735569066987));
#26574=CARTESIAN_POINT('',(0.,0.211787305230605,1.76735569066987));
#26575=CARTESIAN_POINT('Origin',(0.,-0.216927431261162,1.76673214992155));
#26576=CARTESIAN_POINT('',(0.,-0.216927431261162,1.76673214992155));
#26577=CARTESIAN_POINT('',(0.,-0.216927431261162,1.76673214992155));
#26578=CARTESIAN_POINT('',(12.,-0.216927431261162,1.76673214992155));
#26579=CARTESIAN_POINT('',(12.,-0.216927431261162,1.76673214992155));
#26580=CARTESIAN_POINT('',(0.,-0.216927431261162,1.76673214992155));
#26581=CARTESIAN_POINT('Origin',(0.,-0.63305835603048,1.6636216871212));
#26582=CARTESIAN_POINT('',(0.,-0.63305835603048,1.6636216871212));
#26583=CARTESIAN_POINT('',(0.,-0.63305835603048,1.6636216871212));
#26584=CARTESIAN_POINT('',(12.,-0.63305835603048,1.6636216871212));
#26585=CARTESIAN_POINT('',(12.,-0.63305835603048,1.6636216871212));
#26586=CARTESIAN_POINT('',(0.,-0.63305835603048,1.6636216871212));
#26587=CARTESIAN_POINT('Origin',(0.,-1.01246599912308,1.46400566959958));
#26588=CARTESIAN_POINT('',(0.,-1.01246599912308,1.46400566959958));
#26589=CARTESIAN_POINT('',(0.,-1.01246599912308,1.46400566959958));
#26590=CARTESIAN_POINT('',(12.,-1.01246599912308,1.46400566959958));
#26591=CARTESIAN_POINT('',(12.,-1.01246599912308,1.46400566959958));
#26592=CARTESIAN_POINT('',(0.,-1.01246599912308,1.46400566959958));
#26593=CARTESIAN_POINT('Origin',(0.,-1.33314118300442,1.17946368582401));
#26594=CARTESIAN_POINT('',(0.,-1.33314118300442,1.17946368582401));
#26595=CARTESIAN_POINT('',(0.,-1.33314118300442,1.17946368582401));
#26596=CARTESIAN_POINT('',(12.,-1.33314118300442,1.17946368582401));
#26597=CARTESIAN_POINT('',(12.,-1.33314118300442,1.17946368582401));
#26598=CARTESIAN_POINT('',(0.,-1.33314118300442,1.17946368582401));
#26599=CARTESIAN_POINT('Origin',(0.,-1.5764817598753,0.826501821401781));
#26600=CARTESIAN_POINT('',(0.,-1.5764817598753,0.826501821401781));
#26601=CARTESIAN_POINT('',(0.,-1.5764817598753,0.826501821401781));
#26602=CARTESIAN_POINT('',(12.,-1.57648175987531,0.826501821401781));
#26603=CARTESIAN_POINT('',(12.,-1.5764817598753,0.826501821401781));
#26604=CARTESIAN_POINT('',(0.,-1.5764817598753,0.826501821401781));
#26605=CARTESIAN_POINT('Origin',(0.,-1.72837170952577,0.425595152358411));
#26606=CARTESIAN_POINT('',(0.,-1.72837170952577,0.425595152358411));
#26607=CARTESIAN_POINT('',(0.,-1.72837170952577,0.425595152358411));
#26608=CARTESIAN_POINT('',(12.,-1.72837170952577,0.425595152358411));
#26609=CARTESIAN_POINT('',(12.,-1.72837170952577,0.425595152358411));
#26610=CARTESIAN_POINT('',(0.,-1.72837170952577,0.425595152358411));
#26611=CARTESIAN_POINT('Origin',(0.,-1.78,1.00846592378134E-15));
#26612=CARTESIAN_POINT('',(0.,-1.78,1.00846592378134E-15));
#26613=CARTESIAN_POINT('',(0.,-1.78,1.00846592378134E-15));
#26614=CARTESIAN_POINT('',(12.,-1.78,1.04083408558608E-15));
#26615=CARTESIAN_POINT('',(12.,-1.78,1.00846592378134E-15));
#26616=CARTESIAN_POINT('',(0.,-1.78,1.00846592378134E-15));
#26617=CARTESIAN_POINT('Origin',(0.,-1.72837170952577,-0.42559515235841));
#26618=CARTESIAN_POINT('',(0.,-1.72837170952577,-0.42559515235841));
#26619=CARTESIAN_POINT('',(0.,-1.72837170952577,-0.42559515235841));
#26620=CARTESIAN_POINT('',(12.,-1.72837170952577,-0.42559515235841));
#26621=CARTESIAN_POINT('',(12.,-1.72837170952577,-0.42559515235841));
#26622=CARTESIAN_POINT('',(0.,-1.72837170952577,-0.42559515235841));
#26623=CARTESIAN_POINT('Origin',(0.,-1.57648175987531,-0.826501821401781));
#26624=CARTESIAN_POINT('',(0.,-1.57648175987531,-0.826501821401781));
#26625=CARTESIAN_POINT('',(0.,-1.57648175987531,-0.826501821401781));
#26626=CARTESIAN_POINT('',(12.,-1.57648175987531,-0.826501821401781));
#26627=CARTESIAN_POINT('',(12.,-1.57648175987531,-0.826501821401781));
#26628=CARTESIAN_POINT('',(0.,-1.57648175987531,-0.826501821401781));
#26629=CARTESIAN_POINT('Origin',(0.,-1.33314118300442,-1.17946368582401));
#26630=CARTESIAN_POINT('',(0.,-1.33314118300442,-1.17946368582401));
#26631=CARTESIAN_POINT('',(0.,-1.33314118300442,-1.17946368582401));
#26632=CARTESIAN_POINT('',(12.,-1.33314118300442,-1.17946368582401));
#26633=CARTESIAN_POINT('',(12.,-1.33314118300442,-1.17946368582401));
#26634=CARTESIAN_POINT('',(0.,-1.33314118300442,-1.17946368582401));
#26635=CARTESIAN_POINT('Origin',(0.,-1.01246599912308,-1.46400566959958));
#26636=CARTESIAN_POINT('',(0.,-1.01246599912308,-1.46400566959958));
#26637=CARTESIAN_POINT('',(0.,-1.01246599912308,-1.46400566959958));
#26638=CARTESIAN_POINT('',(12.,-1.01246599912308,-1.46400566959958));
#26639=CARTESIAN_POINT('',(12.,-1.01246599912308,-1.46400566959958));
#26640=CARTESIAN_POINT('',(0.,-1.01246599912308,-1.46400566959958));
#26641=CARTESIAN_POINT('Origin',(0.,-0.63305835603048,-1.6636216871212));
#26642=CARTESIAN_POINT('',(0.,-0.63305835603048,-1.6636216871212));
#26643=CARTESIAN_POINT('',(0.,-0.63305835603048,-1.6636216871212));
#26644=CARTESIAN_POINT('',(12.,-0.63305835603048,-1.6636216871212));
#26645=CARTESIAN_POINT('',(12.,-0.63305835603048,-1.6636216871212));
#26646=CARTESIAN_POINT('',(0.,-0.63305835603048,-1.6636216871212));
#26647=CARTESIAN_POINT('Origin',(0.,-0.216927431261162,-1.76673214992155));
#26648=CARTESIAN_POINT('',(0.,-0.216927431261162,-1.76673214992155));
#26649=CARTESIAN_POINT('',(0.,-0.216927431261162,-1.76673214992155));
#26650=CARTESIAN_POINT('',(12.,-0.216927431261162,-1.76673214992155));
#26651=CARTESIAN_POINT('',(12.,-0.216927431261162,-1.76673214992155));
#26652=CARTESIAN_POINT('',(0.,-0.216927431261162,-1.76673214992155));
#26653=CARTESIAN_POINT('Origin',(0.,0.211787305230605,-1.76735569066987));
#26654=CARTESIAN_POINT('',(0.,0.211787305230605,-1.76735569066987));
#26655=CARTESIAN_POINT('',(0.,0.211787305230605,-1.76735569066987));
#26656=CARTESIAN_POINT('',(12.,0.211787305230605,-1.76735569066987));
#26657=CARTESIAN_POINT('',(12.,0.211787305230605,-1.76735569066987));
#26658=CARTESIAN_POINT('',(0.,0.211787305230605,-1.76735569066987));
#26659=CARTESIAN_POINT('Origin',(0.,0.628216405190687,-1.66545613819437));
#26660=CARTESIAN_POINT('',(0.,0.628216405190687,-1.66545613819437));
#26661=CARTESIAN_POINT('',(0.,0.628216405190687,-1.66545613819437));
#26662=CARTESIAN_POINT('',(12.,0.628216405190687,-1.66545613819437));
#26663=CARTESIAN_POINT('',(12.,0.628216405190687,-1.66545613819437));
#26664=CARTESIAN_POINT('',(0.,0.628216405190687,-1.66545613819437));
#26665=CARTESIAN_POINT('Origin',(0.,1.0082031017262,-1.46694461574719));
#26666=CARTESIAN_POINT('',(0.,1.0082031017262,-1.46694461574719));
#26667=CARTESIAN_POINT('',(0.,1.0082031017262,-1.46694461574719));
#26668=CARTESIAN_POINT('',(12.,1.0082031017262,-1.46694461574719));
#26669=CARTESIAN_POINT('',(12.,1.0082031017262,-1.46694461574719));
#26670=CARTESIAN_POINT('',(0.,1.0082031017262,-1.46694461574719));
#26671=CARTESIAN_POINT('Origin',(0.,1.32970462680897,-1.18333664079281));
#26672=CARTESIAN_POINT('',(0.,1.32970462680897,-1.18333664079281));
#26673=CARTESIAN_POINT('',(0.,1.32970462680897,-1.18333664079281));
#26674=CARTESIAN_POINT('',(12.,1.32970462680897,-1.18333664079281));
#26675=CARTESIAN_POINT('',(12.,1.32970462680897,-1.18333664079281));
#26676=CARTESIAN_POINT('',(0.,1.32970462680897,-1.18333664079281));
#26677=CARTESIAN_POINT('Origin',(0.,1.57407089715261,-0.83108411772646));
#26678=CARTESIAN_POINT('',(0.,1.57407089715261,-0.83108411772646));
#26679=CARTESIAN_POINT('',(0.,1.57407089715261,-0.83108411772646));
#26680=CARTESIAN_POINT('',(12.,1.57407089715261,-0.83108411772646));
#26681=CARTESIAN_POINT('',(12.,1.57407089715261,-0.83108411772646));
#26682=CARTESIAN_POINT('',(0.,1.57407089715261,-0.83108411772646));
#26683=CARTESIAN_POINT('Origin',(0.,1.72712639277127,-0.43062097416741));
#26684=CARTESIAN_POINT('',(0.,1.72712639277127,-0.43062097416741));
#26685=CARTESIAN_POINT('',(0.,1.72712639277127,-0.43062097416741));
#26686=CARTESIAN_POINT('',(12.,1.72712639277127,-0.43062097416741));
#26687=CARTESIAN_POINT('',(12.,1.72712639277127,-0.43062097416741));
#26688=CARTESIAN_POINT('',(0.,1.72712639277127,-0.43062097416741));
#26689=CARTESIAN_POINT('Origin',(0.,2.30930382853687,-0.575774111527212));
#26690=CARTESIAN_POINT('',(0.,2.30930382853687,-0.575774111527212));
#26691=CARTESIAN_POINT('',(0.,2.30930382853687,-0.575774111527212));
#26692=CARTESIAN_POINT('',(12.,2.30930382853687,-0.575774111527212));
#26693=CARTESIAN_POINT('',(12.,2.30930382853687,-0.575774111527212));
#26694=CARTESIAN_POINT('',(0.,2.30930382853687,-0.575774111527212));
#26695=CARTESIAN_POINT('Origin',(0.,2.10465659282203,-1.11122483156684));
#26696=CARTESIAN_POINT('',(0.,2.10465659282203,-1.11122483156684));
#26697=CARTESIAN_POINT('',(0.,2.10465659282203,-1.11122483156684));
#26698=CARTESIAN_POINT('',(12.,2.10465659282203,-1.11122483156684));
#26699=CARTESIAN_POINT('',(12.,2.10465659282203,-1.11122483156684));
#26700=CARTESIAN_POINT('',(0.,2.10465659282203,-1.11122483156684));
#26701=CARTESIAN_POINT('Origin',(0.,1.77791966955357,-1.58221416016117));
#26702=CARTESIAN_POINT('',(0.,1.77791966955357,-1.58221416016117));
#26703=CARTESIAN_POINT('',(0.,1.77791966955357,-1.58221416016117));
#26704=CARTESIAN_POINT('',(12.,1.77791966955357,-1.58221416016117));
#26705=CARTESIAN_POINT('',(12.,1.77791966955357,-1.58221416016117));
#26706=CARTESIAN_POINT('',(0.,1.77791966955357,-1.58221416016117));
#26707=CARTESIAN_POINT('Origin',(0.,1.3480468438811,-1.9614203289204));
#26708=CARTESIAN_POINT('',(0.,1.3480468438811,-1.9614203289204));
#26709=CARTESIAN_POINT('',(0.,1.3480468438811,-1.9614203289204));
#26710=CARTESIAN_POINT('',(12.,1.3480468438811,-1.9614203289204));
#26711=CARTESIAN_POINT('',(12.,1.3480468438811,-1.9614203289204));
#26712=CARTESIAN_POINT('',(0.,1.3480468438811,-1.9614203289204));
#26713=CARTESIAN_POINT('Origin',(0.,0.839974744019008,-2.22684584769808));
#26714=CARTESIAN_POINT('',(0.,0.839974744019008,-2.22684584769808));
#26715=CARTESIAN_POINT('',(0.,0.839974744019008,-2.22684584769808));
#26716=CARTESIAN_POINT('',(12.,0.839974744019008,-2.22684584769808));
#26717=CARTESIAN_POINT('',(12.,0.839974744019008,-2.22684584769808));
#26718=CARTESIAN_POINT('',(0.,0.839974744019008,-2.22684584769808));
#26719=CARTESIAN_POINT('Origin',(0.,0.28317628452182,-2.36309356392937));
#26720=CARTESIAN_POINT('',(0.,0.28317628452182,-2.36309356392937));
#26721=CARTESIAN_POINT('',(0.,0.28317628452182,-2.36309356392937));
#26722=CARTESIAN_POINT('',(12.,0.28317628452182,-2.36309356392937));
#26723=CARTESIAN_POINT('',(12.,0.28317628452182,-2.36309356392937));
#26724=CARTESIAN_POINT('',(0.,0.28317628452182,-2.36309356392937));
#26725=CARTESIAN_POINT('Origin',(0.,-0.29004903730425,-2.36225984090635));
#26726=CARTESIAN_POINT('',(0.,-0.29004903730425,-2.36225984090635));
#26727=CARTESIAN_POINT('',(0.,-0.29004903730425,-2.36225984090635));
#26728=CARTESIAN_POINT('',(12.,-0.29004903730425,-2.36225984090635));
#26729=CARTESIAN_POINT('',(12.,-0.29004903730425,-2.36225984090635));
#26730=CARTESIAN_POINT('',(0.,-0.29004903730425,-2.36225984090635));
#26731=CARTESIAN_POINT('Origin',(0.,-0.846448813119406,-2.22439304233059));
#26732=CARTESIAN_POINT('',(0.,-0.846448813119406,-2.22439304233059));
#26733=CARTESIAN_POINT('',(0.,-0.846448813119406,-2.22439304233059));
#26734=CARTESIAN_POINT('',(12.,-0.846448813119406,-2.22439304233059));
#26735=CARTESIAN_POINT('',(12.,-0.846448813119406,-2.22439304233059));
#26736=CARTESIAN_POINT('',(0.,-0.846448813119406,-2.22439304233059));
#26737=CARTESIAN_POINT('Origin',(0.,-1.35374667298479,-1.95749072676798));
#26738=CARTESIAN_POINT('',(0.,-1.35374667298479,-1.95749072676798));
#26739=CARTESIAN_POINT('',(0.,-1.35374667298479,-1.95749072676798));
#26740=CARTESIAN_POINT('',(12.,-1.35374667298479,-1.95749072676798));
#26741=CARTESIAN_POINT('',(12.,-1.35374667298479,-1.95749072676798));
#26742=CARTESIAN_POINT('',(0.,-1.35374667298479,-1.95749072676798));
#26743=CARTESIAN_POINT('Origin',(0.,-1.78251461547782,-1.57703571475346));
#26744=CARTESIAN_POINT('',(0.,-1.78251461547782,-1.57703571475346));
#26745=CARTESIAN_POINT('',(0.,-1.78251461547782,-1.57703571475346));
#26746=CARTESIAN_POINT('',(12.,-1.78251461547782,-1.57703571475346));
#26747=CARTESIAN_POINT('',(12.,-1.78251461547782,-1.57703571475346));
#26748=CARTESIAN_POINT('',(0.,-1.78251461547782,-1.57703571475346));
#26749=CARTESIAN_POINT('Origin',(0.,-2.10788010590069,-1.10509794097542));
#26750=CARTESIAN_POINT('',(0.,-2.10788010590069,-1.10509794097542));
#26751=CARTESIAN_POINT('',(0.,-2.10788010590069,-1.10509794097542));
#26752=CARTESIAN_POINT('',(12.,-2.10788010590069,-1.10509794097541));
#26753=CARTESIAN_POINT('',(12.,-2.10788010590069,-1.10509794097542));
#26754=CARTESIAN_POINT('',(0.,-2.10788010590069,-1.10509794097542));
#26755=CARTESIAN_POINT('Origin',(0.,-2.31096891498389,-0.569054192479223));
#26756=CARTESIAN_POINT('',(0.,-2.31096891498389,-0.569054192479223));
#26757=CARTESIAN_POINT('',(0.,-2.31096891498389,-0.569054192479223));
#26758=CARTESIAN_POINT('',(12.,-2.31096891498389,-0.569054192479223));
#26759=CARTESIAN_POINT('',(12.,-2.31096891498389,-0.569054192479223));
#26760=CARTESIAN_POINT('',(0.,-2.31096891498389,-0.569054192479223));
#26761=CARTESIAN_POINT('Origin',(0.,-2.38,1.34839825764022E-15));
#26762=CARTESIAN_POINT('',(0.,-2.38,1.34839825764022E-15));
#26763=CARTESIAN_POINT('',(0.,-2.38,1.34839825764022E-15));
#26764=CARTESIAN_POINT('',(12.,-2.38,1.31838984174237E-15));
#26765=CARTESIAN_POINT('',(12.,-2.38,1.34839825764022E-15));
#26766=CARTESIAN_POINT('',(0.,-2.38,1.34839825764022E-15));
#26767=CARTESIAN_POINT('Origin',(0.,-2.31096891498389,0.569054192479223));
#26768=CARTESIAN_POINT('',(0.,-2.31096891498389,0.569054192479223));
#26769=CARTESIAN_POINT('',(0.,-2.31096891498389,0.569054192479223));
#26770=CARTESIAN_POINT('',(12.,-2.31096891498389,0.569054192479223));
#26771=CARTESIAN_POINT('',(12.,-2.31096891498389,0.569054192479223));
#26772=CARTESIAN_POINT('',(0.,-2.31096891498389,0.569054192479223));
#26773=CARTESIAN_POINT('Origin',(0.,-2.10788010590069,1.10509794097542));
#26774=CARTESIAN_POINT('',(0.,-2.10788010590069,1.10509794097542));
#26775=CARTESIAN_POINT('',(0.,-2.10788010590069,1.10509794097542));
#26776=CARTESIAN_POINT('',(12.,-2.10788010590069,1.10509794097542));
#26777=CARTESIAN_POINT('',(12.,-2.10788010590069,1.10509794097542));
#26778=CARTESIAN_POINT('',(0.,-2.10788010590069,1.10509794097542));
#26779=CARTESIAN_POINT('Origin',(0.,-1.78251461547783,1.57703571475345));
#26780=CARTESIAN_POINT('',(0.,-1.78251461547783,1.57703571475345));
#26781=CARTESIAN_POINT('',(0.,-1.78251461547783,1.57703571475345));
#26782=CARTESIAN_POINT('',(12.,-1.78251461547783,1.57703571475345));
#26783=CARTESIAN_POINT('',(12.,-1.78251461547783,1.57703571475345));
#26784=CARTESIAN_POINT('',(0.,-1.78251461547783,1.57703571475345));
#26785=CARTESIAN_POINT('Origin',(0.,-1.35374667298479,1.95749072676798));
#26786=CARTESIAN_POINT('',(0.,-1.35374667298479,1.95749072676798));
#26787=CARTESIAN_POINT('',(0.,-1.35374667298479,1.95749072676798));
#26788=CARTESIAN_POINT('',(12.,-1.35374667298479,1.95749072676798));
#26789=CARTESIAN_POINT('',(12.,-1.35374667298479,1.95749072676798));
#26790=CARTESIAN_POINT('',(0.,-1.35374667298479,1.95749072676798));
#26791=CARTESIAN_POINT('Origin',(0.,-0.846448813119406,2.22439304233059));
#26792=CARTESIAN_POINT('',(0.,-0.846448813119406,2.22439304233059));
#26793=CARTESIAN_POINT('',(0.,-0.846448813119406,2.22439304233059));
#26794=CARTESIAN_POINT('',(12.,-0.846448813119405,2.22439304233059));
#26795=CARTESIAN_POINT('',(12.,-0.846448813119406,2.22439304233059));
#26796=CARTESIAN_POINT('',(0.,-0.846448813119406,2.22439304233059));
#26797=CARTESIAN_POINT('Origin',(0.,-0.290049037304251,2.36225984090635));
#26798=CARTESIAN_POINT('',(0.,-0.290049037304251,2.36225984090635));
#26799=CARTESIAN_POINT('',(0.,-0.290049037304251,2.36225984090635));
#26800=CARTESIAN_POINT('',(12.,-0.290049037304251,2.36225984090635));
#26801=CARTESIAN_POINT('',(12.,-0.290049037304251,2.36225984090635));
#26802=CARTESIAN_POINT('',(0.,-0.290049037304251,2.36225984090635));
#26803=CARTESIAN_POINT('Origin',(0.,0.283176284521821,2.36309356392937));
#26804=CARTESIAN_POINT('',(0.,0.283176284521821,2.36309356392937));
#26805=CARTESIAN_POINT('',(0.,0.283176284521821,2.36309356392937));
#26806=CARTESIAN_POINT('',(12.,0.283176284521821,2.36309356392937));
#26807=CARTESIAN_POINT('',(12.,0.283176284521821,2.36309356392937));
#26808=CARTESIAN_POINT('',(0.,0.283176284521821,2.36309356392937));
#26809=CARTESIAN_POINT('Origin',(0.,0.839974744019008,2.22684584769809));
#26810=CARTESIAN_POINT('',(0.,0.839974744019008,2.22684584769809));
#26811=CARTESIAN_POINT('',(0.,0.839974744019008,2.22684584769809));
#26812=CARTESIAN_POINT('',(12.,0.839974744019008,2.22684584769809));
#26813=CARTESIAN_POINT('',(12.,0.839974744019008,2.22684584769809));
#26814=CARTESIAN_POINT('',(0.,0.839974744019008,2.22684584769809));
#26815=CARTESIAN_POINT('Origin',(0.,1.3480468438811,1.9614203289204));
#26816=CARTESIAN_POINT('',(0.,1.3480468438811,1.9614203289204));
#26817=CARTESIAN_POINT('',(0.,1.3480468438811,1.9614203289204));
#26818=CARTESIAN_POINT('',(12.,1.3480468438811,1.9614203289204));
#26819=CARTESIAN_POINT('',(12.,1.3480468438811,1.9614203289204));
#26820=CARTESIAN_POINT('',(0.,1.3480468438811,1.9614203289204));
#26821=CARTESIAN_POINT('Origin',(0.,1.77791966955357,1.58221416016117));
#26822=CARTESIAN_POINT('',(0.,1.77791966955357,1.58221416016117));
#26823=CARTESIAN_POINT('',(0.,1.77791966955357,1.58221416016117));
#26824=CARTESIAN_POINT('',(12.,1.77791966955357,1.58221416016117));
#26825=CARTESIAN_POINT('',(12.,1.77791966955357,1.58221416016117));
#26826=CARTESIAN_POINT('',(0.,1.77791966955357,1.58221416016117));
#26827=CARTESIAN_POINT('Origin',(0.,2.10465659282203,1.11122483156684));
#26828=CARTESIAN_POINT('',(0.,2.10465659282203,1.11122483156684));
#26829=CARTESIAN_POINT('',(0.,2.10465659282203,1.11122483156684));
#26830=CARTESIAN_POINT('',(12.,2.10465659282203,1.11122483156684));
#26831=CARTESIAN_POINT('',(12.,2.10465659282203,1.11122483156684));
#26832=CARTESIAN_POINT('',(0.,2.10465659282203,1.11122483156684));
#26833=CARTESIAN_POINT('Origin',(0.,2.30930382853687,0.575774111527209));
#26834=CARTESIAN_POINT('',(0.,2.30930382853687,0.575774111527209));
#26835=CARTESIAN_POINT('',(0.,2.30930382853687,0.575774111527209));
#26836=CARTESIAN_POINT('',(12.,2.30930382853687,0.575774111527209));
#26837=CARTESIAN_POINT('',(12.,2.30930382853687,0.575774111527209));
#26838=CARTESIAN_POINT('',(0.,2.30930382853687,0.575774111527209));
#26839=CARTESIAN_POINT('Origin',(0.,1.72712639277127,0.430620974167409));
#26840=CARTESIAN_POINT('',(0.,1.72712639277127,0.430620974167409));
#26841=CARTESIAN_POINT('',(12.,1.72712639277127,0.430620974167409));
#26842=CARTESIAN_POINT('Origin',(12.,-0.0353480857315641,0.));
#26843=CARTESIAN_POINT('Origin',(0.,-0.0353480857315641,0.));
#32289=UNCERTAINTY_MEASURE_WITH_UNIT(LENGTH_MEASURE(0.01),#32310,
'DISTANCE_ACCURACY_VALUE',
'Maximum model space distance between geometric entities at asserted c
onnectivities');
#32293=UNCERTAINTY_MEASURE_WITH_UNIT(LENGTH_MEASURE(0.01),#32310,
'DISTANCE_ACCURACY_VALUE',
'Maximum model space distance between geometric entities at asserted c
onnectivities');
#32305=(
GEOMETRIC_REPRESENTATION_CONTEXT(3)
GLOBAL_UNCERTAINTY_ASSIGNED_CONTEXT((#32289))
GLOBAL_UNIT_ASSIGNED_CONTEXT((#32310,#32312,#32313))
REPRESENTATION_CONTEXT('','3D')
);
#32309=(
GEOMETRIC_REPRESENTATION_CONTEXT(3)
GLOBAL_UNCERTAINTY_ASSIGNED_CONTEXT((#32293))
GLOBAL_UNIT_ASSIGNED_CONTEXT((#32310,#32312,#32313))
REPRESENTATION_CONTEXT('','3D')
);
#32310=(
LENGTH_UNIT()
NAMED_UNIT(*)
SI_UNIT(.MILLI.,.METRE.)
);
#32312=(
NAMED_UNIT(*)
PLANE_ANGLE_UNIT()
SI_UNIT($,.RADIAN.)
);
#32313=(
NAMED_UNIT(*)
SI_UNIT($,.STERADIAN.)
SOLID_ANGLE_UNIT()
);
#32325=SHAPE_DEFINITION_REPRESENTATION(#32340,#32372);
#32340=PRODUCT_DEFINITION_SHAPE('',$,#32388);
#32372=SHAPE_REPRESENTATION('',(#14637),#32305);
#32376=PRODUCT_DEFINITION_CONTEXT('part definition',#32423,'design');
#32388=PRODUCT_DEFINITION('2026-10-25-00-35-20-799',
'12_Spring_Pin_ISO_8752_4.76x12',#32403,#32376);
#32403=PRODUCT_DEFINITION_FORMATION('',$,#32436);
#32423=APPLICATION_CONTEXT(
'Core Data for Automotive Mechanical Design Process');
#32424=PRODUCT_CONTEXT('part definition',#32423,'mechanical');
#32436=PRODUCT('2026-10-25-00-35-20-799',
'12_Spring_Pin_ISO_8752_4.76x12',$,(#32424));
#32496=COLOUR_RGB('Grey',0.48,0.52,0.57);
#32497=FILL_AREA_STYLE_COLOUR('',#32496);
#32498=FILL_AREA_STYLE('',(#32497));
#32499=SURFACE_STYLE_FILL_AREA(#32498);
#32500=SURFACE_SIDE_STYLE('',(#32499));
#32501=SURFACE_STYLE_USAGE(.BOTH.,#32500);
#32502=PRESENTATION_STYLE_ASSIGNMENT((#32501));
ENDSEC;
END-ISO-10303-21;
